ISO-10303-21;
HEADER;
FILE_DESCRIPTION (('STEP AP203'),
    '1' );
FILE_NAME ('bench vise10-.step',
    '2026-10-07T23:37:23',
    ( '' ),
    ( '' ),
    'SwSTEP 2.0',
    'SolidWorks 2024',
    '' );
FILE_SCHEMA (( 'AUTOMOTIVE_DESIGN' ));
ENDSEC;

DATA;
#28=AXIS2_PLACEMENT_3D ( 'NONE', #2617, #7646, #6878 ) ;
#33=( BOUNDED_SURFACE ( )  B_SPLINE_SURFACE ( 3, 3, ( 
 ( #3117, #4870, #7402, #4254 ),
 ( #5609, #6767, #8175, #1152 ),
 ( #198, #3878, #2545, #7053 ),
 ( #4418, #1438, #7009, #3230 ),
 ( #1275, #1924, #4991, #5814 ),
 ( #6924, #3192, #7610, #6392 ) ),
 .UNSPECIFIED., .F., .F., .F. ) 
 B_SPLINE_SURFACE_WITH_KNOTS ( ( 4, 2, 4 ),
 ( 4, 4 ),
 ( 0.000000000000000000, 0.5000000000000000000, 1.000000000000000000 ),
 ( 0.000000000000000000, 1.000000000000000000 ),
 .UNSPECIFIED. ) 
 GEOMETRIC_REPRESENTATION_ITEM ( )  RATIONAL_B_SPLINE_SURFACE ( (
 ( 1.000000000000000000, 0.3333333333333334259, 0.3333333333333334259, 1.000000000000000000),
 ( 1.000000000000000000, 0.3333333333333334259, 0.3333333333333334259, 1.000000000000000000),
 ( 1.000000000000000000, 0.3333333333333334259, 0.3333333333333334259, 1.000000000000000000),
 ( 1.000000000000000000, 0.3333333333333334259, 0.3333333333333334259, 1.000000000000000000),
 ( 1.000000000000000000, 0.3333333333333334259, 0.3333333333333334259, 1.000000000000000000),
 ( 1.000000000000000000, 0.3333333333333334259, 0.3333333333333334259, 1.000000000000000000) ) ) 
 REPRESENTATION_ITEM ( '' )  SURFACE ( )  );
#41=VERTEX_POINT ( 'NONE', #2074 ) ;
#44=AXIS2_PLACEMENT_3D ( 'NONE', #2089, #4037, #244 ) ;
#45=CARTESIAN_POINT ( 'NONE',  ( 3.987953385826772390, 3.755224612465394962, 8.262149156879575074 ) ) ;
#52=CARTESIAN_POINT ( 'NONE',  ( 4.462953385826772035, 3.753500037802128375, 8.231249998505111520 ) ) ;
#63=CARTESIAN_POINT ( 'NONE',  ( -3.987046614173229919, 3.872296061808612411, 8.050752829671743882 ) ) ;
#65=ORIENTED_EDGE ( 'NONE', *, *, #1296, .T. ) ;
#72=AXIS2_PLACEMENT_3D ( 'NONE', #6327, #85, #2600 ) ;
#74=CARTESIAN_POINT ( 'NONE',  ( -4.462046614173229564, 3.753500037802127043, 8.231249998505111520 ) ) ;
#85=DIRECTION ( 'NONE',  ( -1.000000000000000000, 0.000000000000000000, 0.000000000000000000 ) ) ;
#87=CARTESIAN_POINT ( 'NONE',  ( 3.987953385826771946, 3.763524128032369465, 8.293365503768654889 ) ) ;
#105=CARTESIAN_POINT ( 'NONE',  ( -3.987046614173230363, 4.023873226579398832, 8.413336896757355632 ) ) ;
#116=PLANE ( 'NONE',  #837 ) ;
#119=ORIENTED_EDGE ( 'NONE', *, *, #2557, .F. ) ;
#125=CARTESIAN_POINT ( 'NONE',  ( 3.987953385826773278, 3.848025092515661161, 8.399350079849197570 ) ) ;
#138=CARTESIAN_POINT ( 'NONE',  ( 3.987953385826772390, 4.262500003889283740, 8.231249998505111520 ) ) ;
#143=CARTESIAN_POINT ( 'NONE',  ( 4.476342532109287120, 3.950000015938371689, 8.543749986456024459 ) ) ;
#145=CARTESIAN_POINT ( 'NONE',  ( -3.987046614173229475, 3.767882598671322913, 8.305060267424060783 ) ) ;
#167=CARTESIAN_POINT ( 'NONE',  ( 3.987953385826771946, 3.848075132174967550, 8.063218304144973203 ) ) ;
#171=CARTESIAN_POINT ( 'NONE',  ( 3.987953385826772834, 4.017233591675260840, 8.415903052206910928 ) ) ;
#193=CARTESIAN_POINT ( 'NONE',  ( -3.987046614173227699, 4.110686350265323696, 8.118096427185742314 ) ) ;
#196=CARTESIAN_POINT ( 'NONE',  ( -3.987046614173228143, 3.937513178174820716, 8.427751303491342938 ) ) ;
#197=ORIENTED_EDGE ( 'NONE', *, *, #7668, .T. ) ;
#198=CARTESIAN_POINT ( 'NONE',  ( -4.382879947506562068, 3.516000035344543306, 8.231249998505111520 ) ) ;
#217=CARTESIAN_POINT ( 'NONE',  ( 3.987953385826772834, 3.831130030893720395, 8.074194664662527998 ) ) ;
#218=CARTESIAN_POINT ( 'NONE',  ( 4.383786719160104539, 3.516000035344543750, 8.231249998505111520 ) ) ;
#220=CARTESIAN_POINT ( 'NONE',  ( 3.987953385826771946, 3.876943811450185962, 8.413666033243973885 ) ) ;
#231=VERTEX_POINT ( 'NONE', #2199 ) ;
#242=CARTESIAN_POINT ( 'NONE',  ( -3.987046614173229475, 3.771838453700684379, 8.314258565286809954 ) ) ;
#244=DIRECTION ( 'NONE',  ( 0.000000000000000000, 0.000000000000000000, 1.000000000000000000 ) ) ;
#254=( NAMED_UNIT ( * ) PLANE_ANGLE_UNIT ( ) SI_UNIT ( $, .RADIAN. ) );
#280=CARTESIAN_POINT ( 'NONE',  ( -3.987046614173229475, 4.146499994074616779, 8.243740188835159799 ) ) ;
#287=ORIENTED_EDGE ( 'NONE', *, *, #4323, .T. ) ;
#298=CARTESIAN_POINT ( 'NONE',  ( 4.067120052493439886, 3.516000035344541974, 7.363250037317452090 ) ) ;
#300=CARTESIAN_POINT ( 'NONE',  ( 3.987953385826772390, 3.980893307323090546, 8.426027723965566096 ) ) ;
#312=CARTESIAN_POINT ( 'NONE',  ( 4.383786719160104539, 3.516000035344543750, 8.231249998505111520 ) ) ;
#315=ORIENTED_EDGE ( 'NONE', *, *, #879, .T. ) ;
#330=CARTESIAN_POINT ( 'NONE',  ( -4.462046614173229564, 4.146499994074616779, 8.231249998505111520 ) ) ;
#335=ORIENTED_EDGE ( 'NONE', *, *, #5247, .F. ) ;
#338=CARTESIAN_POINT ( 'NONE',  ( 3.987953385826771946, 3.674333370316265945, 8.231249998505111520 ) ) ;
#348=AXIS2_PLACEMENT_3D ( 'NONE', #5515, #2418, #7445 ) ;
#349=EDGE_LOOP ( 'NONE', ( #4385, #197 ) ) ;
#386=CARTESIAN_POINT ( 'NONE',  ( -3.987046614173228587, 4.001800847919961157, 8.041502862977342403 ) ) ;
#426=CARTESIAN_POINT ( 'NONE',  ( -3.987046614173228587, 4.068870000982347968, 8.074194664662202925 ) ) ;
#440=CARTESIAN_POINT ( 'NONE',  ( -3.987046614173229031, 4.146499994074616779, 7.838250042232624004 ) ) ;
#451=CARTESIAN_POINT ( 'NONE',  ( -4.462046614173230452, 4.225666661560478765, 8.231249998505111520 ) ) ;
#456=( GEOMETRIC_REPRESENTATION_CONTEXT ( 3 ) GLOBAL_UNCERTAINTY_ASSIGNED_CONTEXT ( ( #7884 ) ) GLOBAL_UNIT_ASSIGNED_CONTEXT ( ( #4708, #254, #948 ) ) REPRESENTATION_CONTEXT ( 'NONE', 'WORKASPACE' ) );
#458=ORIENTED_EDGE ( 'NONE', *, *, #3599, .F. ) ;
#483=CARTESIAN_POINT ( 'NONE',  ( -4.462046614173229564, 4.146499994074616779, 8.231249998505111520 ) ) ;
#508=CARTESIAN_POINT ( 'NONE',  ( 3.987953385826772390, 4.118031710298198256, 8.129325114741229541 ) ) ;
#519=CARTESIAN_POINT ( 'NONE',  ( -4.382879947506562068, 3.516000035344543306, 8.231249998505111520 ) ) ;
#538=EDGE_CURVE ( 'NONE', #2664, #6568, #3093, .T. ) ;
#556=DIRECTION ( 'NONE',  ( 0.000000000000000000, 0.000000000000000000, 1.000000000000000000 ) ) ;
#559=AXIS2_PLACEMENT_3D ( 'NONE', #8173, #1922, #3228 ) ;
#612=CARTESIAN_POINT ( 'NONE',  ( -3.987046614173229475, 3.753500037802127931, 8.218759808176336890 ) ) ;
#626=CARTESIAN_POINT ( 'NONE',  ( 4.383786719160104539, 4.383999996532199184, 8.231249998505111520 ) ) ;
#650=CARTESIAN_POINT ( 'NONE',  ( -3.987046614173228587, 3.781968321577594772, 8.129325114742682601 ) ) ;
#687=CARTESIAN_POINT ( 'NONE',  ( -3.987046614173228587, 3.848025092515166001, 8.063149917161112512 ) ) ;
#708=ORIENTED_EDGE ( 'NONE', *, *, #1597, .F. ) ;
#711=CARTESIAN_POINT ( 'NONE',  ( 3.987953385826773278, 3.768538842735476457, 8.155839089539284714 ) ) ;
#736=CARTESIAN_POINT ( 'NONE',  ( -4.462046614173229564, 3.753500037802127043, 8.231249998505111520 ) ) ;
#749=FACE_BOUND ( 'NONE', #349, .T. ) ;
#754=CARTESIAN_POINT ( 'NONE',  ( 3.987953385826771946, 3.776897850680958513, 8.137838423720895165 ) ) ;
#773=CARTESIAN_POINT ( 'NONE',  ( -3.987046614173229475, 4.144775419411349304, 8.262149156880317591 ) ) ;
#790=CARTESIAN_POINT ( 'NONE',  ( 3.987953385826772834, 3.862475978536469068, 8.055097764145562778 ) ) ;
#806=CARTESIAN_POINT ( 'NONE',  ( -3.987046614173228587, 4.118100097282441752, 8.129275075082505353 ) ) ;
#808=CARTESIAN_POINT ( 'NONE',  ( -3.987046614173229475, 4.043411590721250448, 8.404352163763398664 ) ) ;
#820=CIRCLE ( 'NONE', #5530, 0.3124999879509117728 ) ;
#829=CARTESIAN_POINT ( 'NONE',  ( 3.987953385826771946, 4.225666661560476989, 7.679916707260901809 ) ) ;
#832=CARTESIAN_POINT ( 'NONE',  ( -4.462046614173229564, 4.146499994074616779, 8.231249998505111520 ) ) ;
#837=AXIS2_PLACEMENT_3D ( 'NONE', #3529, #1073, #949 ) ;
#853=CARTESIAN_POINT ( 'NONE',  ( -3.987046614173228587, 3.806261876195067728, 8.365405826660635924 ) ) ;
#877=CARTESIAN_POINT ( 'NONE',  ( 3.987953385826772390, 4.143082812052599984, 8.267743937948607069 ) ) ;
#879=EDGE_CURVE ( 'NONE', #41, #5506, #3278, .T. ) ;
#915=CARTESIAN_POINT ( 'NONE',  ( 3.987953385826771946, 4.146499994074615891, 8.231249998505111520 ) ) ;
#919=CARTESIAN_POINT ( 'NONE',  ( 3.987953385826772834, 4.112654374748815123, 8.341552593656999193 ) ) ;
#935=CARTESIAN_POINT ( 'NONE',  ( -3.987046614173229919, 4.133273763909712351, 8.302127249793111119 ) ) ;
#947=B_SPLINE_CURVE_WITH_KNOTS ( 'NONE', 3,
 ( #5498, #8149, #3779, #4348, #2484, #7548, #1129, #6200, #1896, #3164, #2447, #6856, #508, #5539, #8061, #2397, #1854, #7426, #1785, #8107, #4469, #3290, #5169, #1325, #7628, #4431, #4512, #3928, #1981, #7067, #1942, #7028, #6325, #6368, #4598, #6939, #6982, #7108, #4557, #790, #5788, #167, #2019, #217, #1371, #3813, #7752, #1452, #1495, #6453, #3854, #754, #1414, #2597, #711, #3247, #2558, #6410, #2719, #5126, #5090, #3206, #5876, #5048, #5207, #5750 ),
 .UNSPECIFIED., .F., .F.,
 ( 4, 1, 1, 1, 1, 2, 2, 1, 2, 2, 2, 1, 2, 2, 1, 1, 1, 2, 2, 2, 1, 1, 1, 1, 2, 2, 1, 2, 2, 2, 1, 2, 2, 1, 1, 2, 2, 1, 1, 1, 2, 2, 4 ),
 ( 0.000000000000000000, 0.06249999999998323563, 0.09374999999997758737, 0.1093749999999724942, 0.1171874999999721056, 0.1210937499999718975, 0.1249999999999717171, 0.1562499999999758249, 0.1718749999999749922, 0.1874999999999741596, 0.2499999999999581446, 0.2812499999999501510, 0.2968749999999454880, 0.3124999999999408806, 0.3437499999999316658, 0.3593749999999270028, 0.3671874999999247269, 0.3710937499999257816, 0.3749999999999268363, 0.4999999999999173994, 0.5624999999999127365, 0.5937499999999102940, 0.6093749999999091838, 0.6171874999999095168, 0.6210937499999082956, 0.6249999999999071854, 0.6562499999999119593, 0.6718749999999144018, 0.6874999999999167333, 0.7499999999999256151, 0.7812499999999300559, 0.7968749999999323874, 0.8124999999999346079, 0.8437499999999376055, 0.8593749999999362732, 0.8671874999999384936, 0.8749999999999407141, 0.9062499999999484857, 0.9218749999999550360, 0.9296874999999605871, 0.9335937499999659162, 0.9374999999999713562, 1.000000000000000000 ),
 .UNSPECIFIED. ) ;
#948=( NAMED_UNIT ( * ) SI_UNIT ( $, .STERADIAN. ) SOLID_ANGLE_UNIT ( ) );
#949=DIRECTION ( 'NONE',  ( 0.000000000000000000, 0.000000000000000000, 1.000000000000000000 ) ) ;
#959=ADVANCED_FACE ( 'N', ( #2980 ), #4782, .T. ) ;
#962=CARTESIAN_POINT ( 'NONE',  ( 3.987953385826772390, 4.051924899703798211, 8.399281692864075666 ) ) ;
#964=AXIS2_PLACEMENT_3D ( 'NONE', #138, #4485, #3348 ) ;
#967=CARTESIAN_POINT ( 'NONE',  ( -3.987046614173228587, 4.130163526686910558, 8.152788242568700383 ) ) ;
#984=ORIENTED_EDGE ( 'NONE', *, *, #7546, .F. ) ;
#1008=CARTESIAN_POINT ( 'NONE',  ( -3.987046614173228587, 4.079363137579387733, 8.082722253684375247 ) ) ;
#1019=VECTOR ( 'NONE', #3073, 39.37007874015748143 ) ;
#1051=CARTESIAN_POINT ( 'NONE',  ( -3.987046614173229475, 4.020876854703656633, 8.047976087269148593 ) ) ;
#1068=CYLINDRICAL_SURFACE ( 'NONE', #348, 0.3124999879509117728 ) ;
#1073=DIRECTION ( 'NONE',  ( -1.000000000000000000, 0.000000000000000000, 0.000000000000000000 ) ) ;
#1076=CARTESIAN_POINT ( 'NONE',  ( -4.462046614173229564, 4.146499994075096396, 7.838250042231664771 ) ) ;
#1083=ORIENTED_EDGE ( 'NONE', *, *, #2557, .T. ) ;
#1102=CARTESIAN_POINT ( 'NONE',  ( 4.383786719160104539, 3.516000035344543750, 8.231249998505111520 ) ) ;
#1103=B_SPLINE_CURVE_WITH_KNOTS ( 'NONE', 3,
 ( #5274, #4045, #6687, #6065, #451, #330 ),
 .UNSPECIFIED., .F., .F.,
 ( 4, 2, 4 ),
 ( 0.000000000000000000, 0.5000000000000000000, 1.000000000000000000 ),
 .UNSPECIFIED. ) ;
#1112=( BOUNDED_CURVE ( )  B_SPLINE_CURVE ( 3, ( #5649, #7059, #1443, #74 ),
 .UNSPECIFIED., .F., .F. ) 
 B_SPLINE_CURVE_WITH_KNOTS ( ( 4, 4 ),
 ( 0.000000000000000000, 1.000000000000000000 ),
 .UNSPECIFIED. ) 
 CURVE ( )  GEOMETRIC_REPRESENTATION_ITEM ( )  RATIONAL_B_SPLINE_CURVE ( ( 1.000000000000000000, 0.3333333333333334259, 0.3333333333333334259, 1.000000000000000000 ) ) 
 REPRESENTATION_ITEM ( '' )  );
#1127=B_SPLINE_CURVE_WITH_KNOTS ( 'NONE', 3,
 ( #1436, #280, #773, #6431, #7733, #5146, #3876, #935, #4035, #7171, #2046, #6567, #7770, #4613, #5225, #2774, #2087, #7051, #7648, #5262, #1471, #7818, #808, #6390, #3396, #4577, #105, #3271, #5893, #5189, #196, #6477, #2619, #4494, #7087, #7007, #1516, #4540, #2167, #4655, #1394, #1555, #5771, #3945, #2738, #853, #3354, #5812, #7127, #5860, #4000, #2705, #242, #6526, #7694, #145, #3910, #3308, #2122, #2661, #5540, #5461, #4852, #3665, #4349, #4891 ),
 .UNSPECIFIED., .F., .F.,
 ( 4, 1, 1, 1, 1, 2, 2, 1, 2, 2, 2, 1, 2, 2, 1, 1, 1, 2, 2, 2, 1, 1, 1, 1, 2, 2, 1, 2, 2, 2, 1, 2, 2, 1, 1, 2, 2, 1, 1, 1, 2, 2, 4 ),
 ( 0.000000000000000000, 0.06250000000002353673, 0.09375000000003830269, 0.1093750000000430211, 0.1171875000000484335, 0.1210937500000485584, 0.1250000000000486833, 0.1562500000000372757, 0.1718750000000286715, 0.1875000000000200673, 0.2499999999999983347, 0.2812499999999865663, 0.2968749999999816813, 0.3124999999999767963, 0.3437499999999648614, 0.3593749999999588662, 0.3671874999999570344, 0.3710937499999559241, 0.3749999999999548694, 0.4999999999999330536, 0.5624999999999207301, 0.5937499999999150679, 0.6093749999999122924, 0.6171874999999112932, 0.6210937499999130695, 0.6249999999999147349, 0.6562499999999166223, 0.6718749999999176215, 0.6874999999999186207, 0.7499999999999197309, 0.7812499999999220623, 0.7968749999999220623, 0.8124999999999220623, 0.8437499999999235056, 0.8593749999999270583, 0.8671874999999292788, 0.8749999999999316103, 0.9062499999999429345, 0.9218749999999511502, 0.9296874999999525935, 0.9335937499999537037, 0.9374999999999547029, 1.000000000000000000 ),
 .UNSPECIFIED. ) ;
#1129=CARTESIAN_POINT ( 'NONE',  ( 3.987953385826773278, 4.133830657811393472, 8.161828647664988168 ) ) ;
#1152=CARTESIAN_POINT ( 'NONE',  ( -4.462046614173230452, 4.225666661560478765, 8.231249998505111520 ) ) ;
#1176=CARTESIAN_POINT ( 'NONE',  ( -3.987046614173228587, 3.674333370316265945, 8.231249998505111520 ) ) ;
#1179=FACE_OUTER_BOUND ( 'NONE', #3877, .T. ) ;
#1211=CARTESIAN_POINT ( 'NONE',  ( -4.066213280839894750, 3.516000035344541530, 7.363250037317452090 ) ) ;
#1271=CARTESIAN_POINT ( 'NONE',  ( -3.987046614173228587, 3.778630425947245186, 8.135040162507303663 ) ) ;
#1275=CARTESIAN_POINT ( 'NONE',  ( -3.987046614173228587, 3.674333370316265945, 8.231249998505111520 ) ) ;
#1296=EDGE_CURVE ( 'NONE', #2207, #7215, #6652, .T. ) ;
#1305=CARTESIAN_POINT ( 'NONE',  ( -3.987046614173228587, 3.831386823445361856, 8.074548610981766572 ) ) ;
#1307=CARTESIAN_POINT ( 'NONE',  ( -4.382879947506562068, 3.516000035344543306, 8.231249998505111520 ) ) ;
#1318=CARTESIAN_POINT ( 'NONE',  ( 4.462953385826772035, 4.146499994074615003, 8.231249998505111520 ) ) ;
#1325=CARTESIAN_POINT ( 'NONE',  ( 3.987953385826772834, 4.033008582717783952, 8.053088436265779748 ) ) ;
#1371=CARTESIAN_POINT ( 'NONE',  ( 3.987953385826772834, 3.820636894297861019, 8.082722253683524372 ) ) ;
#1394=CARTESIAN_POINT ( 'NONE',  ( -3.987046614173229475, 3.853790179936717575, 8.402619588493877245 ) ) ;
#1395=ORIENTED_EDGE ( 'NONE', *, *, #1296, .F. ) ;
#1414=CARTESIAN_POINT ( 'NONE',  ( 3.987953385826771946, 3.771838453699690508, 8.148241431725164574 ) ) ;
#1416=CARTESIAN_POINT ( 'NONE',  ( 3.987953385826772390, 3.856588441155107017, 8.404352163763244121 ) ) ;
#1436=CARTESIAN_POINT ( 'NONE',  ( -3.987046614173228587, 4.146499994074616779, 8.231249998505111520 ) ) ;
#1438=CARTESIAN_POINT ( 'NONE',  ( -4.066213280839894750, 3.516000035344541530, 9.099249959692773615 ) ) ;
#1443=CARTESIAN_POINT ( 'NONE',  ( -4.462046614173229564, 3.753500037801645206, 8.624249954778562710 ) ) ;
#1450=EDGE_LOOP ( 'NONE', ( #5896, #6287, #119, #4407 ) ) ;
#1452=CARTESIAN_POINT ( 'NONE',  ( 3.987953385826772390, 3.793298628413402263, 8.112636806013968638 ) ) ;
#1455=CARTESIAN_POINT ( 'NONE',  ( 3.987953385826772834, 3.900888680988107371, 8.423148454254921091 ) ) ;
#1466=CARTESIAN_POINT ( 'NONE',  ( 3.987953385826772390, 3.753500037802128375, 8.231249998505111520 ) ) ;
#1471=CARTESIAN_POINT ( 'NONE',  ( -3.987046614173228587, 4.060302611091305636, 8.393904357314925235 ) ) ;
#1495=CARTESIAN_POINT ( 'NONE',  ( 3.987953385826771058, 3.789313681611198970, 8.118096427186111796 ) ) ;
#1496=CARTESIAN_POINT ( 'NONE',  ( 4.462953385826771147, 3.753500037802127931, 8.231249998505111520 ) ) ;
#1516=CARTESIAN_POINT ( 'NONE',  ( -3.987046614173228587, 3.879123177173203540, 8.414523909741193464 ) ) ;
#1530=ORIENTED_EDGE ( 'NONE', *, *, #4992, .F. ) ;
#1541=CARTESIAN_POINT ( 'NONE',  ( 3.987953385826772390, 4.123102181194456151, 8.324661573291658456 ) ) ;
#1554=ORIENTED_EDGE ( 'NONE', *, *, #7424, .T. ) ;
#1555=CARTESIAN_POINT ( 'NONE',  ( -3.987046614173228587, 3.848075132173495394, 8.399281692864384752 ) ) ;
#1574=CARTESIAN_POINT ( 'NONE',  ( 3.987953385826771946, 3.753500037802127931, 8.231249998505111520 ) ) ;
#1576=CARTESIAN_POINT ( 'NONE',  ( 3.987953385826772390, 4.146499994074615003, 8.231249998505111520 ) ) ;
#1597=EDGE_CURVE ( 'NONE', #6568, #3656, #2507, .T. ) ;
#1601=VERTEX_POINT ( 'NONE', #7496 ) ;
#1616=CARTESIAN_POINT ( 'NONE',  ( 3.987953385826771946, 4.118100097281283567, 8.333224921929698326 ) ) ;
#1634=ORIENTED_EDGE ( 'NONE', *, *, #7668, .F. ) ;
#1659=CARTESIAN_POINT ( 'NONE',  ( -3.987046614173228587, 4.106701403462994726, 8.112636806013382440 ) ) ;
#1684=APPLICATION_CONTEXT ( 'configuration controlled 3d designs of mechanical parts and assemblies' ) ;
#1714=CARTESIAN_POINT ( 'NONE',  ( -4.066213280839896527, 4.383999996532201848, 8.231249998505111520 ) ) ;
#1757=CARTESIAN_POINT ( 'NONE',  ( 3.987953385826771946, 3.674333370316266389, 8.231249998505111520 ) ) ;
#1785=CARTESIAN_POINT ( 'NONE',  ( 3.987953385826772390, 4.068613208430805095, 8.074548610981311825 ) ) ;
#1797=CARTESIAN_POINT ( 'NONE',  ( -4.462046614173229564, 4.146499994074616779, 7.838250042232624004 ) ) ;
#1831=EDGE_LOOP ( 'NONE', ( #7332, #315, #3326, #1083 ) ) ;
#1854=CARTESIAN_POINT ( 'NONE',  ( 3.987953385826771946, 4.084155844093235288, 8.087511858761496697 ) ) ;
#1878=CARTESIAN_POINT ( 'NONE',  ( -3.987046614173229475, 3.769737734435318899, 8.152751440555805473 ) ) ;
#1896=CARTESIAN_POINT ( 'NONE',  ( 3.987953385826772390, 4.133008534184493321, 8.159690390570387919 ) ) ;
#1920=CARTESIAN_POINT ( 'NONE',  ( -3.987046614173228587, 3.783676849830932110, 8.126559114045873500 ) ) ;
#1922=DIRECTION ( 'NONE',  ( -1.000000000000000000, 0.000000000000000000, 0.000000000000000000 ) ) ;
#1924=CARTESIAN_POINT ( 'NONE',  ( -3.987046614173229031, 3.674333370316265501, 8.782583289749323896 ) ) ;
#1933=CARTESIAN_POINT ( 'NONE',  ( 4.462953385826772035, 4.146499994074615003, 8.231249998505111520 ) ) ;
#1942=CARTESIAN_POINT ( 'NONE',  ( 3.987953385826773278, 3.937513178173875250, 8.034748693519857099 ) ) ;
#1947=CARTESIAN_POINT ( 'NONE',  ( 3.987953385826772834, 3.769737734436292342, 8.309748556456428403 ) ) ;
#1970=EDGE_CURVE ( 'NONE', #2664, #7024, #6430, .T. ) ;
#1981=CARTESIAN_POINT ( 'NONE',  ( 3.987953385826772390, 3.999111350882339266, 8.039351542753342628 ) ) ;
#2019=CARTESIAN_POINT ( 'NONE',  ( 3.987953385826772834, 3.845309131479383247, 8.064926832397505407 ) ) ;
#2023=CARTESIAN_POINT ( 'NONE',  ( 3.987953385826772834, 3.823364637257239185, 8.381772284350258673 ) ) ;
#2040=( BOUNDED_CURVE ( )  B_SPLINE_CURVE ( 3, ( #6337, #2650, #5133, #52 ),
 .UNSPECIFIED., .F., .F. ) 
 B_SPLINE_CURVE_WITH_KNOTS ( ( 4, 4 ),
 ( 0.000000000000000000, 1.000000000000000000 ),
 .UNSPECIFIED. ) 
 CURVE ( )  GEOMETRIC_REPRESENTATION_ITEM ( )  RATIONAL_B_SPLINE_CURVE ( ( 1.000000000000000000, 0.3333333333333334259, 0.3333333333333334259, 1.000000000000000000 ) ) 
 REPRESENTATION_ITEM ( '' )  );
#2043=CARTESIAN_POINT ( 'NONE',  ( -3.987046614173230363, 3.766726267967030140, 8.160372747217270017 ) ) ;
#2046=CARTESIAN_POINT ( 'NONE',  ( -3.987046614173229475, 4.126152250297099755, 8.318774035909180853 ) ) ;
#2056=AXIS2_PLACEMENT_3D ( 'NONE', #3481, #4862, #7309 ) ;
#2061=SHAPE_REPRESENTATION_RELATIONSHIP ( 'NONE' , 'NONE' ,  #7355, #7953 ) ;
#2070=CARTESIAN_POINT ( 'NONE',  ( 3.987953385826772834, 4.128161578176055002, 8.314258565286806402 ) ) ;
#2074=CARTESIAN_POINT ( 'NONE',  ( 4.462953385826772035, 4.146499994074615003, 8.231249998505111520 ) ) ;
#2081=CARTESIAN_POINT ( 'NONE',  ( 3.987953385826771946, 3.674333370316266389, 8.231249998505111520 ) ) ;
#2087=CARTESIAN_POINT ( 'NONE',  ( -3.987046614173229475, 4.084155844094571997, 8.374988138248092184 ) ) ;
#2089=CARTESIAN_POINT ( 'NONE',  ( -3.987046614173228587, 3.950000015938371689, 8.231249998505111520 ) ) ;
#2107=CARTESIAN_POINT ( 'NONE',  ( 4.462953385826773811, 4.225666661560476989, 7.679916707260901809 ) ) ;
#2108=CARTESIAN_POINT ( 'NONE',  ( 3.987953385826773278, 4.110686350264241895, 8.344403569825947997 ) ) ;
#2122=CARTESIAN_POINT ( 'NONE',  ( -3.987046614173228587, 3.759071817854777287, 8.277905906474869013 ) ) ;
#2145=CARTESIAN_POINT ( 'NONE',  ( 3.987953385826772390, 4.019420561376718659, 8.415080959133108607 ) ) ;
#2167=CARTESIAN_POINT ( 'NONE',  ( -3.987046614173229475, 3.871501457986266104, 8.411512280006446574 ) ) ;
#2191=CARTESIAN_POINT ( 'NONE',  ( 3.987953385826771946, 3.753500037802127931, 7.838250042232624892 ) ) ;
#2193=CARTESIAN_POINT ( 'NONE',  ( 3.987953385826772390, 4.068870000980494339, 8.388305332349000665 ) ) ;
#2195=ORIENTED_EDGE ( 'NONE', *, *, #1597, .T. ) ;
#2197=CARTESIAN_POINT ( 'NONE',  ( -3.987046614173229475, 4.142924502496678762, 8.193927407620929415 ) ) ;
#2199=CARTESIAN_POINT ( 'NONE',  ( -3.987046614173228587, 4.146499994074616779, 8.231249998505111520 ) ) ;
#2207=VERTEX_POINT ( 'NONE', #7516 ) ;
#2266=CARTESIAN_POINT ( 'NONE',  ( -3.987046614173228587, 4.100522301784816470, 8.104614619825735389 ) ) ;
#2282=CARTESIAN_POINT ( 'NONE',  ( -4.382879947506561180, 4.383999996532200960, 7.363250037317454755 ) ) ;
#2292=CIRCLE ( 'NONE', #44, 0.3124999879509117728 ) ;
#2305=EDGE_CURVE ( 'NONE', #231, #7215, #1103, .T. ) ;
#2317=CARTESIAN_POINT ( 'NONE',  ( -3.987046614173228143, 4.131461189141452550, 8.155839089539586695 ) ) ;
#2334=CARTESIAN_POINT ( 'NONE',  ( 3.987953385826771946, 3.674333370316267278, 8.782583289749323896 ) ) ;
#2348=CARTESIAN_POINT ( 'NONE',  ( -4.462046614173229564, 3.753500037802127043, 8.231249998505111520 ) ) ;
#2379=ADVANCED_FACE ( 'NONE', ( #3525 ), #1068, .T. ) ;
#2393=CARTESIAN_POINT ( 'NONE',  ( -3.987046614173228587, 3.950000015938371689, 8.231249998505111520 ) ) ;
#2397=CARTESIAN_POINT ( 'NONE',  ( 3.987953385826771946, 4.098527760758083893, 8.101886876862897324 ) ) ;
#2412=CARTESIAN_POINT ( 'NONE',  ( -4.462046614173230452, 4.225666661560478765, 8.231249998505111520 ) ) ;
#2418=DIRECTION ( 'NONE',  ( -1.000000000000000000, 0.000000000000000000, 0.000000000000000000 ) ) ;
#2447=CARTESIAN_POINT ( 'NONE',  ( 3.987953385826772834, 4.126152250297301372, 8.143725961102258992 ) ) ;
#2464=CARTESIAN_POINT ( 'NONE',  ( 4.462953385826772923, 3.674333370316267278, 8.782583289749323896 ) ) ;
#2484=CARTESIAN_POINT ( 'NONE',  ( 3.987953385826772390, 4.136475903844373470, 8.169134493240660433 ) ) ;
#2491=CARTESIAN_POINT ( 'NONE',  ( 3.987953385826773278, 3.792944682096142550, 8.350119983549243230 ) ) ;
#2497=CARTESIAN_POINT ( 'NONE',  ( 4.067120052493439886, 3.516000035344543306, 8.231249998505111520 ) ) ;
#2507=LINE ( 'NONE', #3121, #1019 ) ;
#2522=CARTESIAN_POINT ( 'NONE',  ( 3.987953385826772834, 3.753500037802127931, 8.243740188834737026 ) ) ;
#2540=CARTESIAN_POINT ( 'NONE',  ( -3.987046614173228143, 3.815844187783087094, 8.087511858761828876 ) ) ;
#2545=CARTESIAN_POINT ( 'NONE',  ( -4.382879947506561180, 4.383999996532200960, 9.099249959692771839 ) ) ;
#2557=EDGE_CURVE ( 'NONE', #6895, #3907, #5692, .T. ) ;
#2558=CARTESIAN_POINT ( 'NONE',  ( 3.987953385826772390, 3.764952780855910675, 8.164838062276935204 ) ) ;
#2563=CARTESIAN_POINT ( 'NONE',  ( 3.987953385826772834, 3.760254621899925542, 8.283055230728429308 ) ) ;
#2578=CARTESIAN_POINT ( 'NONE',  ( -3.987046614173228143, 3.874591561940378792, 8.049793446537691466 ) ) ;
#2580=CARTESIAN_POINT ( 'NONE',  ( -3.987046614173228587, 3.674333370316265945, 8.231249998505111520 ) ) ;
#2591=B_SPLINE_CURVE_WITH_KNOTS ( 'NONE', 3,
 ( #5627, #2522, #45, #2563, #87, #8155, #5054, #3860, #7594, #1947, #6371, #6944, #2602, #7669, #2491, #3253, #5092, #2023, #4519, #7631, #5757, #125, #1416, #5210, #6588, #4058, #5791, #220, #1455, #4640, #5329, #300, #7154, #5290, #171, #2145, #7844, #7195, #6504, #2804, #2685, #962, #5173, #2193, #7716, #4021, #6548, #2722, #2108, #919, #1616, #1541, #2070, #4561, #7069, #4680, #7114, #3932, #3456, #5958, #3417, #5912, #877, #5880, #6457, #1576 ),
 .UNSPECIFIED., .F., .F.,
 ( 4, 1, 1, 1, 1, 2, 2, 1, 2, 2, 2, 1, 2, 2, 1, 1, 1, 2, 2, 2, 1, 1, 1, 1, 2, 2, 1, 2, 2, 2, 1, 2, 2, 1, 1, 2, 2, 1, 1, 1, 2, 2, 4 ),
 ( 0.000000000000000000, 0.06249999999999043820, 0.09374999999998293032, 0.1093749999999795441, 0.1171874999999774070, 0.1210937499999789196, 0.1249999999999804323, 0.1562499999999877598, 0.1718749999999885369, 0.1874999999999892863, 0.2499999999999923950, 0.2812499999999912847, 0.2968749999999907296, 0.3124999999999901745, 0.3437499999999868994, 0.3593749999999852340, 0.3671874999999832356, 0.3710937499999822364, 0.3749999999999812372, 0.4999999999999621414, 0.5624999999999512612, 0.5937499999999463762, 0.6093749999999424904, 0.6171874999999398259, 0.6210937499999392708, 0.6249999999999388267, 0.6562499999999519273, 0.6718749999999595879, 0.6874999999999673594, 0.7499999999999937828, 0.7812500000000061062, 0.7968750000000112133, 0.8125000000000162093, 0.8437500000000262013, 0.8593750000000284217, 0.8671875000000294209, 0.8750000000000304201, 0.9062500000000217604, 0.9218750000000145439, 0.9296875000000108802, 0.9335937500000087708, 0.9375000000000065503, 1.000000000000000000 ),
 .UNSPECIFIED. ) ;
#2597=CARTESIAN_POINT ( 'NONE',  ( 3.987953385826773278, 3.769836505190169884, 8.152788242568149712 ) ) ;
#2600=DIRECTION ( 'NONE',  ( 0.000000000000000000, 0.000000000000000000, 1.000000000000000000 ) ) ;
#2602=CARTESIAN_POINT ( 'NONE',  ( 3.987953385826771058, 3.781968321578446979, 8.333174882269297257 ) ) ;
#2617=CARTESIAN_POINT ( 'NONE',  ( 3.987953385826772390, 3.950000015938371689, 8.231249998505111520 ) ) ;
#2619=CARTESIAN_POINT ( 'NONE',  ( -3.987046614173229475, 3.898199183958024783, 8.420997134034164944 ) ) ;
#2642=ORIENTED_EDGE ( 'NONE', *, *, #3917, .T. ) ;
#2650=CARTESIAN_POINT ( 'NONE',  ( 4.462953385826771147, 4.146499994075096396, 7.838250042231665660 ) ) ;
#2660=DIRECTION ( 'NONE',  ( -1.000000000000000000, 0.000000000000000000, 0.000000000000000000 ) ) ;
#2661=CARTESIAN_POINT ( 'NONE',  ( -3.987046614173228587, 3.757861515926525176, 8.272475195628263833 ) ) ;
#2664=VERTEX_POINT ( 'NONE', #2700 ) ;
#2670=CARTESIAN_POINT ( 'NONE',  ( 4.462953385826772923, 4.146499994075099060, 8.624249954778562710 ) ) ;
#2673=CIRCLE ( 'NONE', #28, 0.3124999879509117728 ) ;
#2685=CARTESIAN_POINT ( 'NONE',  ( 3.987953385826772390, 4.046209851940893110, 8.402619588493392300 ) ) ;
#2700=CARTESIAN_POINT ( 'NONE',  ( 3.987953385826772390, 3.950000015938371689, 8.543749986456024459 ) ) ;
#2701=MANIFOLD_SOLID_BREP ( 'Imported1', #6743 ) ;
#2703=CARTESIAN_POINT ( 'NONE',  ( -3.987046614173227699, 4.132117433205395152, 8.157439729585876265 ) ) ;
#2705=CARTESIAN_POINT ( 'NONE',  ( -3.987046614173228587, 3.776897850682283231, 8.324661573291654904 ) ) ;
#2719=CARTESIAN_POINT ( 'NONE',  ( 3.987953385826772834, 3.759071817854598763, 8.184594090536538857 ) ) ;
#2720=CARTESIAN_POINT ( 'NONE',  ( 4.067120052493439886, 3.516000035344542862, 8.231249998505111520 ) ) ;
#2722=CARTESIAN_POINT ( 'NONE',  ( 3.987953385826772834, 4.106701403461291200, 8.349863190999146312 ) ) ;
#2734=PLANE ( 'NONE',  #964 ) ;
#2738=CARTESIAN_POINT ( 'NONE',  ( -3.987046614173229475, 3.820636894295539321, 8.379777743323508332 ) ) ;
#2774=CARTESIAN_POINT ( 'NONE',  ( -3.987046614173230363, 4.098527760755414917, 8.360613120148601141 ) ) ;
#2804=CARTESIAN_POINT ( 'NONE',  ( 3.987953385826772390, 4.037524053344319519, 8.407402232862313696 ) ) ;
#2846=CARTESIAN_POINT ( 'NONE',  ( -3.987046614173229475, 4.140928214022093989, 8.184594090536863931 ) ) ;
#2876=( BOUNDED_SURFACE ( )  B_SPLINE_SURFACE ( 3, 3, ( 
 ( #483, #1797, #7387, #4288 ),
 ( #2412, #7944, #7994, #4781 ),
 ( #3641, #2282, #6139, #519 ),
 ( #1714, #3013, #1211, #2979 ),
 ( #7438, #5385, #6679, #1176 ),
 ( #3676, #440, #6755, #6791 ) ),
 .UNSPECIFIED., .F., .F., .F. ) 
 B_SPLINE_SURFACE_WITH_KNOTS ( ( 4, 2, 4 ),
 ( 4, 4 ),
 ( 0.000000000000000000, 0.5000000000000000000, 1.000000000000000000 ),
 ( 0.000000000000000000, 1.000000000000000000 ),
 .UNSPECIFIED. ) 
 GEOMETRIC_REPRESENTATION_ITEM ( )  RATIONAL_B_SPLINE_SURFACE ( (
 ( 1.000000000000000000, 0.3333333333333334259, 0.3333333333333334259, 1.000000000000000000),
 ( 1.000000000000000000, 0.3333333333333334259, 0.3333333333333334259, 1.000000000000000000),
 ( 1.000000000000000000, 0.3333333333333334259, 0.3333333333333334259, 1.000000000000000000),
 ( 1.000000000000000000, 0.3333333333333334259, 0.3333333333333334259, 1.000000000000000000),
 ( 1.000000000000000000, 0.3333333333333334259, 0.3333333333333334259, 1.000000000000000000),
 ( 1.000000000000000000, 0.3333333333333334259, 0.3333333333333334259, 1.000000000000000000) ) ) 
 REPRESENTATION_ITEM ( '' )  SURFACE ( )  );
#2881=EDGE_LOOP ( 'NONE', ( #708, #7493, #6007, #2989 ) ) ;
#2883=CARTESIAN_POINT ( 'NONE',  ( -3.987046614173226811, 3.876126805297171796, 8.049163100252911818 ) ) ;
#2907=CARTESIAN_POINT ( 'NONE',  ( -4.462046614173229564, 4.146499994074616779, 8.231249998505111520 ) ) ;
#2918=CARTESIAN_POINT ( 'NONE',  ( -3.987046614173228587, 4.128161578177576452, 8.148241431726020778 ) ) ;
#2979=CARTESIAN_POINT ( 'NONE',  ( -4.066213280839896527, 3.516000035344541974, 8.231249998505111520 ) ) ;
#2980=FACE_OUTER_BOUND ( 'NONE', #7220, .T. ) ;
#2989=ORIENTED_EDGE ( 'NONE', *, *, #4992, .T. ) ;
#2999=ADVANCED_FACE ( 'NONE', ( #5764, #4609 ), #2734, .T. ) ;
#3013=CARTESIAN_POINT ( 'NONE',  ( -4.066213280839894750, 4.383999996532201848, 7.363250037317452090 ) ) ;
#3073=DIRECTION ( 'NONE',  ( -1.000000000000000000, 0.000000000000000000, 0.000000000000000000 ) ) ;
#3093=CIRCLE ( 'NONE', #72, 0.3124999879509117728 ) ;
#3117=CARTESIAN_POINT ( 'NONE',  ( -4.462046614173229564, 3.753500037802127043, 8.231249998505111520 ) ) ;
#3121=CARTESIAN_POINT ( 'NONE',  ( 4.476342532109287120, 3.950000015938371689, 7.918750010554200358 ) ) ;
#3143=ORIENTED_EDGE ( 'NONE', *, *, #1970, .F. ) ;
#3148=CARTESIAN_POINT ( 'NONE',  ( -3.987046614173228587, 3.792944682095130027, 8.112380013461466532 ) ) ;
#3159=CARTESIAN_POINT ( 'NONE',  ( 3.987953385826772390, 4.146499994074615003, 8.231249998505111520 ) ) ;
#3164=CARTESIAN_POINT ( 'NONE',  ( 3.987953385826771946, 4.130262297440340014, 8.152751440554144580 ) ) ;
#3188=CARTESIAN_POINT ( 'NONE',  ( -3.987046614173228587, 3.856588441154243263, 8.058147833247129910 ) ) ;
#3192=CARTESIAN_POINT ( 'NONE',  ( -3.987046614173229031, 3.753500037802126599, 8.624249954777603477 ) ) ;
#3206=CARTESIAN_POINT ( 'NONE',  ( 3.987953385826771946, 3.757075529380056622, 8.193927407620869019 ) ) ;
#3228=DIRECTION ( 'NONE',  ( 0.000000000000000000, 0.000000000000000000, 1.000000000000000000 ) ) ;
#3230=CARTESIAN_POINT ( 'NONE',  ( -4.066213280839896527, 4.383999996532201848, 8.231249998505111520 ) ) ;
#3241=FACE_OUTER_BOUND ( 'NONE', #6173, .T. ) ;
#3247=CARTESIAN_POINT ( 'NONE',  ( 3.987953385826772834, 3.767882598671357552, 8.157439729585936661 ) ) ;
#3253=CARTESIAN_POINT ( 'NONE',  ( 3.987953385826772834, 3.801472271119643143, 8.360613120147613486 ) ) ;
#3271=CARTESIAN_POINT ( 'NONE',  ( -3.987046614173229919, 4.023056220426558305, 8.413666033243972109 ) ) ;
#3277=ORIENTED_EDGE ( 'NONE', *, *, #538, .F. ) ;
#3278=B_SPLINE_CURVE_WITH_KNOTS ( 'NONE', 3,
 ( #1933, #6275, #626, #8143, #8184, #3159 ),
 .UNSPECIFIED., .F., .F.,
 ( 4, 2, 4 ),
 ( 0.000000000000000000, 0.5000000000000000000, 1.000000000000000000 ),
 .UNSPECIFIED. ) ;
#3290=CARTESIAN_POINT ( 'NONE',  ( 3.987953385826771946, 4.051974939361221217, 8.063149917160938429 ) ) ;
#3305=CARTESIAN_POINT ( 'NONE',  ( -3.987046614173229475, 4.037524053340656671, 8.055097764145708439 ) ) ;
#3308=CARTESIAN_POINT ( 'NONE',  ( -3.987046614173229475, 3.761880377346255244, 8.288651076800222839 ) ) ;
#3326=ORIENTED_EDGE ( 'NONE', *, *, #7196, .F. ) ;
#3332=CARTESIAN_POINT ( 'NONE',  ( 4.067120052493439886, 4.383999996532200960, 7.363250037317452090 ) ) ;
#3348=DIRECTION ( 'NONE',  ( -0.000000000000000000, 0.000000000000000000, -1.000000000000000000 ) ) ;
#3354=CARTESIAN_POINT ( 'NONE',  ( -3.987046614173228587, 3.799477730093518080, 8.357885377186541120 ) ) ;
#3373=CARTESIAN_POINT ( 'NONE',  ( 4.462953385826771147, 4.146499994074615891, 8.231249998505111520 ) ) ;
#3396=CARTESIAN_POINT ( 'NONE',  ( -3.987046614173228143, 4.027703970067585182, 8.411747167338614162 ) ) ;
#3416=CARTESIAN_POINT ( 'NONE',  ( 3.987953385826771946, 4.146499994074616779, 7.838250042232624892 ) ) ;
#3417=CARTESIAN_POINT ( 'NONE',  ( 3.987953385826772834, 4.142615650101508784, 8.270135292618689959 ) ) ;
#3455=CARTESIAN_POINT ( 'NONE',  ( 4.067120052493439886, 4.383999996532201848, 8.231249998505111520 ) ) ;
#3456=CARTESIAN_POINT ( 'NONE',  ( 3.987953385826771946, 4.140928214022170373, 8.277905906474343212 ) ) ;
#3481=CARTESIAN_POINT ( 'NONE',  ( 4.462953385826771147, 4.146499994074615891, 8.231249998505111520 ) ) ;
#3501=FACE_OUTER_BOUND ( 'NONE', #3810, .T. ) ;
#3504=CARTESIAN_POINT ( 'NONE',  ( -3.987046614173228587, 4.093738155682585145, 8.097094170350759512 ) ) ;
#3508=CARTESIAN_POINT ( 'NONE',  ( 3.987953385826772390, 4.146499994074615003, 8.231249998505111520 ) ) ;
#3525=FACE_OUTER_BOUND ( 'NONE', #2881, .T. ) ;
#3529=CARTESIAN_POINT ( 'NONE',  ( -3.987046614173228587, 4.146499994074616779, 8.231249998505111520 ) ) ;
#3540=CARTESIAN_POINT ( 'NONE',  ( -3.987046614173228587, 3.962486853702869016, 8.034748693519857099 ) ) ;
#3556=CARTESIAN_POINT ( 'NONE',  ( 3.987953385826771946, 4.225666661560476101, 8.231249998505111520 ) ) ;
#3584=CARTESIAN_POINT ( 'NONE',  ( -3.987046614173227699, 3.876943811449999888, 8.048833963766311328 ) ) ;
#3599=EDGE_CURVE ( 'NONE', #6568, #2664, #2673, .T. ) ;
#3605=ORIENTED_EDGE ( 'NONE', *, *, #7546, .T. ) ;
#3641=CARTESIAN_POINT ( 'NONE',  ( -4.382879947506562068, 4.383999996532200960, 8.231249998505111520 ) ) ;
#3644=EDGE_CURVE ( 'NONE', #1601, #231, #4848, .T. ) ;
#3645=CARTESIAN_POINT ( 'NONE',  ( 4.383786719160105427, 3.516000035344544639, 9.099249959692768286 ) ) ;
#3656=VERTEX_POINT ( 'NONE', #7200 ) ;
#3661=ORIENTED_EDGE ( 'NONE', *, *, #538, .T. ) ;
#3665=CARTESIAN_POINT ( 'NONE',  ( -3.987046614173228143, 3.754593536049172453, 8.255194476360108169 ) ) ;
#3676=CARTESIAN_POINT ( 'NONE',  ( -3.987046614173228587, 4.146499994074616779, 8.231249998505111520 ) ) ;
#3680=CYLINDRICAL_SURFACE ( 'NONE', #5563, 0.3124999879509117728 ) ;
#3713=ORIENTED_EDGE ( 'NONE', *, *, #7424, .F. ) ;
#3720=CARTESIAN_POINT ( 'NONE',  ( -3.987046614173228587, 3.755224612465394518, 8.200350840132131225 ) ) ;
#3736=CARTESIAN_POINT ( 'NONE',  ( 0.000000000000000000, 0.000000000000000000, 0.000000000000000000 ) ) ;
#3762=DIMENSIONAL_EXPONENTS ( 1.000000000000000000, 0.000000000000000000, 0.000000000000000000, 0.000000000000000000, 0.000000000000000000, 0.000000000000000000, 0.000000000000000000 ) ;
#3763=CARTESIAN_POINT ( 'NONE',  ( -3.987046614173229475, 3.766169374065349906, 8.161828647665473113 ) ) ;
#3779=CARTESIAN_POINT ( 'NONE',  ( 3.987953385826771058, 4.144775419411346640, 8.200350840128573182 ) ) ;
#3791=CARTESIAN_POINT ( 'NONE',  ( 3.987953385826772390, 3.950000015938371689, 7.918750010554200358 ) ) ;
#3796=CARTESIAN_POINT ( 'NONE',  ( -3.987046614173229475, 3.836846444618186691, 8.070563664178971308 ) ) ;
#3810=EDGE_LOOP ( 'NONE', ( #1395, #7962 ) ) ;
#3813=CARTESIAN_POINT ( 'NONE',  ( 3.987953385826772390, 3.806261876193907767, 8.097094170351185838 ) ) ;
#3836=EDGE_LOOP ( 'NONE', ( #3277, #458 ) ) ;
#3854=CARTESIAN_POINT ( 'NONE',  ( 3.987953385826774166, 3.781899934594699975, 8.129275075081856983 ) ) ;
#3860=CARTESIAN_POINT ( 'NONE',  ( 3.987953385826772390, 3.766726267967030140, 8.302127249793056052 ) ) ;
#3876=CARTESIAN_POINT ( 'NONE',  ( -3.987046614173229475, 4.133830657811391696, 8.300671349345057237 ) ) ;
#3877=EDGE_LOOP ( 'NONE', ( #3661, #2195, #1554, #3143 ) ) ;
#3878=CARTESIAN_POINT ( 'NONE',  ( -4.382879947506561180, 3.516000035344543306, 9.099249959692771839 ) ) ;
#3901=CARTESIAN_POINT ( 'NONE',  ( 4.462953385826772923, 4.146499994074616779, 8.624249954777599925 ) ) ;
#3907=VERTEX_POINT ( 'NONE', #4967 ) ;
#3908=CARTESIAN_POINT ( 'NONE',  ( -3.987046614173227699, 3.980893307323864150, 8.036472273046369352 ) ) ;
#3910=CARTESIAN_POINT ( 'NONE',  ( -3.987046614173228587, 3.764952780856046122, 8.297661934734193778 ) ) ;
#3917=EDGE_CURVE ( 'NONE', #5506, #6895, #947, .T. ) ;
#3928=CARTESIAN_POINT ( 'NONE',  ( 3.987953385826772834, 4.023056220426754592, 8.048833963766313104 ) ) ;
#3932=CARTESIAN_POINT ( 'NONE',  ( 3.987953385826772390, 4.138119654530761693, 8.288651076799524731 ) ) ;
#3945=CARTESIAN_POINT ( 'NONE',  ( -3.987046614173229919, 3.831130030895572691, 8.388305332348675591 ) ) ;
#3952=SHAPE_DEFINITION_REPRESENTATION ( #5562, #7355 ) ;
#3976=CARTESIAN_POINT ( 'NONE',  ( 3.987953385826771946, 4.225666661560477877, 8.231249998505111520 ) ) ;
#4000=CARTESIAN_POINT ( 'NONE',  ( -3.987046614173228587, 3.781899934595456259, 8.333224921929698326 ) ) ;
#4019=CARTESIAN_POINT ( 'NONE',  ( 4.383786719160105427, 3.516000035344543306, 7.363250037317454755 ) ) ;
#4021=CARTESIAN_POINT ( 'NONE',  ( 3.987953385826772390, 4.093738155681345248, 8.365405826661140409 ) ) ;
#4035=CARTESIAN_POINT ( 'NONE',  ( -3.987046614173228587, 4.133008534184505756, 8.302809606439751633 ) ) ;
#4037=DIRECTION ( 'NONE',  ( 1.000000000000000000, -0.000000000000000000, -0.000000000000000000 ) ) ;
#4045=CARTESIAN_POINT ( 'NONE',  ( -3.987046614173228587, 4.225666661560477877, 8.231249998505111520 ) ) ;
#4055=CARTESIAN_POINT ( 'NONE',  ( 4.383786719160104539, 4.383999996532200072, 8.231249998505111520 ) ) ;
#4058=CARTESIAN_POINT ( 'NONE',  ( 3.987953385826772390, 3.874591561940604834, 8.412706550472572431 ) ) ;
#4061=CARTESIAN_POINT ( 'NONE',  ( -3.987046614173229475, 4.112654374748236918, 8.120947403352236194 ) ) ;
#4108=CARTESIAN_POINT ( 'NONE',  ( 3.987953385826772390, 3.753500037802128375, 8.231249998505111520 ) ) ;
#4145=EDGE_LOOP ( 'NONE', ( #6493, #7351, #984, #65 ) ) ;
#4159=CARTESIAN_POINT ( 'NONE',  ( 3.987953385826771946, 3.753500037802130596, 8.624249954777599925 ) ) ;
#4199=CARTESIAN_POINT ( 'NONE',  ( 3.987953385826771946, 4.146499994074616779, 8.624249954777599925 ) ) ;
#4217=DIRECTION ( 'NONE',  ( 0.000000000000000000, 0.000000000000000000, 1.000000000000000000 ) ) ;
#4254=CARTESIAN_POINT ( 'NONE',  ( -4.462046614173229564, 4.146499994074616779, 8.231249998505111520 ) ) ;
#4288=CARTESIAN_POINT ( 'NONE',  ( -4.462046614173229564, 3.753500037802127043, 8.231249998505111520 ) ) ;
#4323=EDGE_CURVE ( 'NONE', #7215, #2207, #1112, .T. ) ;
#4329=EDGE_CURVE ( 'NONE', #3907, #41, #5646, .T. ) ;
#4348=CARTESIAN_POINT ( 'NONE',  ( 3.987953385826773278, 4.139745409976817392, 8.179444766280242973 ) ) ;
#4349=CARTESIAN_POINT ( 'NONE',  ( -3.987046614173228587, 3.753500037802127043, 8.243275897753244763 ) ) ;
#4372=CARTESIAN_POINT ( 'NONE',  ( -3.987046614173229475, 3.773847781577545746, 8.143725961105161559 ) ) ;
#4376=CARTESIAN_POINT ( 'NONE',  ( -3.987046614173228587, 3.753500037802127043, 8.231249998505111520 ) ) ;
#4385=ORIENTED_EDGE ( 'NONE', *, *, #3644, .T. ) ;
#4407=ORIENTED_EDGE ( 'NONE', *, *, #3917, .F. ) ;
#4409=CARTESIAN_POINT ( 'NONE',  ( 4.462953385826773811, 4.225666661560476101, 8.231249998505111520 ) ) ;
#4416=CARTESIAN_POINT ( 'NONE',  ( -4.462046614173230452, 3.674333370316265057, 8.231249998505111520 ) ) ;
#4418=CARTESIAN_POINT ( 'NONE',  ( -4.066213280839896527, 3.516000035344541974, 8.231249998505111520 ) ) ;
#4431=CARTESIAN_POINT ( 'NONE',  ( 3.987953385826772834, 4.025408469936202493, 8.049793446537611530 ) ) ;
#4469=CARTESIAN_POINT ( 'NONE',  ( 3.987953385826771946, 4.060302611091127112, 8.068595639695296029 ) ) ;
#4485=DIRECTION ( 'NONE',  ( 1.000000000000000000, 0.000000000000000000, -0.000000000000000000 ) ) ;
#4494=CARTESIAN_POINT ( 'NONE',  ( -3.987046614173228587, 3.887887077483224818, 8.417726902280634249 ) ) ;
#4512=CARTESIAN_POINT ( 'NONE',  ( 3.987953385826771058, 4.023873226579484097, 8.049163100252867409 ) ) ;
#4519=CARTESIAN_POINT ( 'NONE',  ( 3.987953385826772834, 3.831386823445262380, 8.387951386028717593 ) ) ;
#4540=CARTESIAN_POINT ( 'NONE',  ( -3.987046614173228587, 3.878440408003787532, 8.414258516751308647 ) ) ;
#4557=CARTESIAN_POINT ( 'NONE',  ( 3.987953385826772834, 3.871501457987948314, 8.050987717002785260 ) ) ;
#4561=CARTESIAN_POINT ( 'NONE',  ( 3.987953385826772390, 4.130163526685932673, 8.309711754443199538 ) ) ;
#4577=CARTESIAN_POINT ( 'NONE',  ( -3.987046614173227699, 4.025408469936037292, 8.412706550472611511 ) ) ;
#4580=EDGE_LOOP ( 'NONE', ( #2642, #8020 ) ) ;
#4592=( LENGTH_UNIT ( ) NAMED_UNIT ( * ) SI_UNIT ( $, .METRE. ) );
#4598=CARTESIAN_POINT ( 'NONE',  ( 3.987953385826772834, 3.882766440201302682, 8.046596944803717122 ) ) ;
#4609=FACE_BOUND ( 'NONE', #4580, .T. ) ;
#4613=CARTESIAN_POINT ( 'NONE',  ( -3.987046614173228587, 4.116323182045732665, 8.335940882964735010 ) ) ;
#4639=CARTESIAN_POINT ( 'NONE',  ( 4.383786719160105427, 4.383999996532200072, 7.363250037317454755 ) ) ;
#4640=CARTESIAN_POINT ( 'NONE',  ( 3.987953385826773278, 3.925026340410263881, 8.427747322941383956 ) ) ;
#4655=CARTESIAN_POINT ( 'NONE',  ( -3.987046614173229919, 3.862475978533526089, 8.407402232862935421 ) ) ;
#4678=FACE_OUTER_BOUND ( 'NONE', #1450, .T. ) ;
#4680=CARTESIAN_POINT ( 'NONE',  ( 3.987953385826772390, 4.132117433205379164, 8.305060267424163811 ) ) ;
#4682=CARTESIAN_POINT ( 'NONE',  ( -3.987046614173229919, 4.146499994074617668, 8.219224099255814764 ) ) ;
#4708=( CONVERSION_BASED_UNIT ( 'INCH', #7878 ) LENGTH_UNIT ( ) NAMED_UNIT ( #3762 ) );
#4722=CARTESIAN_POINT ( 'NONE',  ( -3.987046614173228143, 4.019420561376825241, 8.047419037877350689 ) ) ;
#4763=CARTESIAN_POINT ( 'NONE',  ( -3.987046614173228587, 4.135047251020795400, 8.164838062277185671 ) ) ;
#4779=ADVANCED_FACE ( 'NONE', ( #5484 ), #33, .T. ) ;
#4781=CARTESIAN_POINT ( 'NONE',  ( -4.462046614173230452, 3.674333370316265057, 8.231249998505111520 ) ) ;
#4782=PLANE ( 'NONE',  #2056 ) ;
#4807=DIRECTION ( 'NONE',  ( 1.000000000000000000, -0.000000000000000000, -0.000000000000000000 ) ) ;
#4810=CARTESIAN_POINT ( 'NONE',  ( -3.987046614173229919, 4.143082812052600872, 8.194756059061747422 ) ) ;
#4828=CARTESIAN_POINT ( 'NONE',  ( 4.383786719160105427, 4.383999996532202736, 9.099249959692766510 ) ) ;
#4848=B_SPLINE_CURVE_WITH_KNOTS ( 'NONE', 3,
 ( #4987, #612, #3720, #5027, #7691, #7526, #3763, #2043, #6263, #1878, #4372, #1271, #650, #1920, #3148, #5639, #2540, #6919, #1305, #3796, #6306, #687, #3188, #5684, #63, #2578, #2883, #3584, #6666, #5372, #3540, #3908, #386, #6045, #5417, #4722, #1051, #6429, #6591, #3305, #5811, #7926, #7976, #426, #1008, #3504, #2266, #1659, #193, #4061, #806, #6004, #2918, #967, #2317, #2703, #4763, #5187, #2846, #7292, #7850, #2197, #4810, #5334, #4682, #7334 ),
 .UNSPECIFIED., .F., .F.,
 ( 4, 1, 1, 1, 1, 2, 2, 1, 2, 2, 2, 1, 2, 2, 1, 1, 1, 2, 2, 2, 1, 1, 1, 1, 2, 2, 1, 2, 2, 2, 1, 2, 2, 1, 1, 2, 2, 1, 1, 1, 2, 2, 4 ),
 ( 0.000000000000000000, 0.06250000000000618949, 0.09375000000000655032, 0.1093750000000071193, 0.1171875000000052458, 0.1210937500000043160, 0.1250000000000033862, 0.1562500000000120737, 0.1718750000000147382, 0.1875000000000174027, 0.2500000000000182077, 0.2812500000000194844, 0.2968750000000217049, 0.3125000000000238698, 0.3437500000000262013, 0.3593750000000273670, 0.3671875000000291434, 0.3710937500000290323, 0.3750000000000289213, 0.4999999999999668043, 0.5624999999999343858, 0.5937499999999176215, 0.6093749999999092948, 0.6171874999999059641, 0.6210937499999055200, 0.6249999999999050759, 0.6562499999998950839, 0.6718749999998911981, 0.6874999999998873124, 0.7499999999998724354, 0.7812499999998641087, 0.7968749999998607780, 0.8124999999998574474, 0.8437499999998507860, 0.8593749999998491207, 0.8671874999998483435, 0.8749999999998474554, 0.9062499999998501199, 0.9218749999998540057, 0.9296874999998562261, 0.9335937499998603339, 0.9374999999998643307, 1.000000000000000000 ),
 .UNSPECIFIED. ) ;
#4852=CARTESIAN_POINT ( 'NONE',  ( -3.987046614173229475, 3.756917219824143395, 8.267743937948555555 ) ) ;
#4862=DIRECTION ( 'NONE',  ( 1.000000000000000000, 0.000000000000000000, -0.000000000000000000 ) ) ;
#4865=CARTESIAN_POINT ( 'NONE',  ( 3.987953385826771946, 4.146499994074615003, 8.231249998505111520 ) ) ;
#4870=CARTESIAN_POINT ( 'NONE',  ( -4.462046614173229564, 3.753500037802126599, 8.624249954777603477 ) ) ;
#4891=CARTESIAN_POINT ( 'NONE',  ( -3.987046614173228587, 3.753500037802127043, 8.231249998505111520 ) ) ;
#4907=CARTESIAN_POINT ( 'NONE',  ( 4.067120052493438997, 4.383999996532202736, 9.099249959692768286 ) ) ;
#4967=CARTESIAN_POINT ( 'NONE',  ( 4.462953385826772035, 3.753500037802128375, 8.231249998505111520 ) ) ;
#4984=CARTESIAN_POINT ( 'NONE',  ( 4.462953385826772923, 4.225666661560477877, 8.782583289749322120 ) ) ;
#4987=CARTESIAN_POINT ( 'NONE',  ( -3.987046614173228587, 3.753500037802127043, 8.231249998505111520 ) ) ;
#4991=CARTESIAN_POINT ( 'NONE',  ( -3.987046614173229031, 4.225666661560476989, 8.782583289749323896 ) ) ;
#4992=EDGE_CURVE ( 'NONE', #7024, #3656, #2292, .T. ) ;
#5027=CARTESIAN_POINT ( 'NONE',  ( -3.987046614173229475, 3.760254621899925542, 8.179444766282907509 ) ) ;
#5048=CARTESIAN_POINT ( 'NONE',  ( 3.987953385826772390, 3.754593536049173341, 8.207305520649800457 ) ) ;
#5054=CARTESIAN_POINT ( 'NONE',  ( 3.987953385826771946, 3.766169374065351239, 8.300671349344955985 ) ) ;
#5069=ADVANCED_FACE ( 'NONE', ( #7820 ), #2876, .T. ) ;
#5090=CARTESIAN_POINT ( 'NONE',  ( 3.987953385826771946, 3.757384381775243920, 8.192364704391765784 ) ) ;
#5092=CARTESIAN_POINT ( 'NONE',  ( 3.987953385826772834, 3.815844187783016483, 8.374988138248586012 ) ) ;
#5126=CARTESIAN_POINT ( 'NONE',  ( 3.987953385826772834, 3.757861515926419482, 8.190024801382651987 ) ) ;
#5133=CARTESIAN_POINT ( 'NONE',  ( 4.462953385826771147, 3.753500037801649203, 7.838250042231665660 ) ) ;
#5146=CARTESIAN_POINT ( 'NONE',  ( -3.987046614173229919, 4.134652525424356462, 8.298484949317895598 ) ) ;
#5169=CARTESIAN_POINT ( 'NONE',  ( 3.987953385826772390, 4.043411590721873061, 8.058147833246822600 ) ) ;
#5173=CARTESIAN_POINT ( 'NONE',  ( 3.987953385826774166, 4.054690900397992515, 8.397573164612390784 ) ) ;
#5181=CARTESIAN_POINT ( 'NONE',  ( 4.462953385826771147, 4.146499994074615003, 8.231249998505111520 ) ) ;
#5187=CARTESIAN_POINT ( 'NONE',  ( -3.987046614173228143, 4.138119654530659552, 8.173848920212014590 ) ) ;
#5189=CARTESIAN_POINT ( 'NONE',  ( -3.987046614173229475, 3.974973691465472747, 8.427747322941382180 ) ) ;
#5207=CARTESIAN_POINT ( 'NONE',  ( 3.987953385826772390, 3.753500037802127931, 8.219224099256663862 ) ) ;
#5209=CARTESIAN_POINT ( 'NONE',  ( 4.462953385826771147, 3.753500037802127931, 7.838250042232624892 ) ) ;
#5210=CARTESIAN_POINT ( 'NONE',  ( 3.987953385826772390, 3.866991449159138394, 8.409411560744331382 ) ) ;
#5225=CARTESIAN_POINT ( 'NONE',  ( -3.987046614173229475, 4.107055349781922438, 8.350119983547221736 ) ) ;
#5244=CARTESIAN_POINT ( 'NONE',  ( 4.462953385826773811, 4.225666661560477877, 8.231249998505111520 ) ) ;
#5246=ORIENTED_EDGE ( 'NONE', *, *, #2305, .T. ) ;
#5247=EDGE_CURVE ( 'NONE', #41, #3907, #2040, .T. ) ;
#5262=CARTESIAN_POINT ( 'NONE',  ( -3.987046614173229475, 4.063153587259359156, 8.391936332830987055 ) ) ;
#5274=CARTESIAN_POINT ( 'NONE',  ( -3.987046614173228587, 4.146499994074616779, 8.231249998505111520 ) ) ;
#5290=CARTESIAN_POINT ( 'NONE',  ( 3.987953385826771058, 4.012112954393902697, 8.417726902280632473 ) ) ;
#5329=CARTESIAN_POINT ( 'NONE',  ( 3.987953385826773278, 3.962486853702427592, 8.427751303491342938 ) ) ;
#5334=CARTESIAN_POINT ( 'NONE',  ( -3.987046614173229475, 4.145406495827572257, 8.207305520648951358 ) ) ;
#5372=CARTESIAN_POINT ( 'NONE',  ( -3.987046614173227699, 3.925026340409374370, 8.034752674066879763 ) ) ;
#5385=CARTESIAN_POINT ( 'NONE',  ( -3.987046614173229031, 4.225666661560476989, 7.679916707260901809 ) ) ;
#5417=CARTESIAN_POINT ( 'NONE',  ( -3.987046614173229475, 4.017233591675442916, 8.046596944803717122 ) ) ;
#5461=CARTESIAN_POINT ( 'NONE',  ( -3.987046614173228143, 3.757075529380089485, 8.268572589389572514 ) ) ;
#5484=FACE_OUTER_BOUND ( 'NONE', #7562, .T. ) ;
#5498=CARTESIAN_POINT ( 'NONE',  ( 3.987953385826772390, 4.146499994074615003, 8.231249998505111520 ) ) ;
#5506=VERTEX_POINT ( 'NONE', #3508 ) ;
#5515=CARTESIAN_POINT ( 'NONE',  ( 4.476342532109287120, 3.950000015938371689, 8.231249998505111520 ) ) ;
#5530=AXIS2_PLACEMENT_3D ( 'NONE', #2393, #4807, #4217 ) ;
#5539=CARTESIAN_POINT ( 'NONE',  ( 3.987953385826772390, 4.116323182045893425, 8.126559114046001397 ) ) ;
#5540=CARTESIAN_POINT ( 'NONE',  ( -3.987046614173228587, 3.757384381775306093, 8.270135292618874701 ) ) ;
#5562=PRODUCT_DEFINITION_SHAPE ( 'NONE', 'NONE',  #6424 ) ;
#5563=AXIS2_PLACEMENT_3D ( 'NONE', #7391, #6175, #556 ) ;
#5609=CARTESIAN_POINT ( 'NONE',  ( -4.462046614173230452, 3.674333370316265057, 8.231249998505111520 ) ) ;
#5618=DIRECTION ( 'NONE',  ( 1.000000000000000000, 0.000000000000000000, 0.000000000000000000 ) ) ;
#5627=CARTESIAN_POINT ( 'NONE',  ( 3.987953385826772390, 3.753500037802128375, 8.231249998505111520 ) ) ;
#5639=CARTESIAN_POINT ( 'NONE',  ( -3.987046614173228143, 3.801472271119497037, 8.101886876862232967 ) ) ;
#5646=( BOUNDED_CURVE ( )  B_SPLINE_CURVE ( 3, ( #6274, #7098, #2670, #1318 ),
 .UNSPECIFIED., .F., .T. ) 
 B_SPLINE_CURVE_WITH_KNOTS ( ( 4, 4 ),
 ( 0.000000000000000000, 1.000000000000000000 ),
 .UNSPECIFIED. ) 
 CURVE ( )  GEOMETRIC_REPRESENTATION_ITEM ( )  RATIONAL_B_SPLINE_CURVE ( ( 1.000000000000000000, 0.3333333333333332038, 0.3333333333333332038, 1.000000000000000000 ) ) 
 REPRESENTATION_ITEM ( '' )  );
#5649=CARTESIAN_POINT ( 'NONE',  ( -4.462046614173229564, 4.146499994074616779, 8.231249998505111520 ) ) ;
#5684=CARTESIAN_POINT ( 'NONE',  ( -3.987046614173229475, 3.866991449158490912, 8.053088436266007122 ) ) ;
#5692=B_SPLINE_CURVE_WITH_KNOTS ( 'NONE', 3,
 ( #1466, #2081, #7765, #312, #7641, #6472 ),
 .UNSPECIFIED., .F., .F.,
 ( 4, 2, 4 ),
 ( 0.000000000000000000, 0.5000000000000000000, 1.000000000000000000 ),
 .UNSPECIFIED. ) ;
#5725=CARTESIAN_POINT ( 'NONE',  ( 4.462953385826772923, 3.753500037802130596, 8.624249954777599925 ) ) ;
#5750=CARTESIAN_POINT ( 'NONE',  ( 3.987953385826772390, 3.753500037802128375, 8.231249998505111520 ) ) ;
#5757=CARTESIAN_POINT ( 'NONE',  ( 3.987953385826773278, 3.839697420785548321, 8.393904357314971421 ) ) ;
#5764=FACE_OUTER_BOUND ( 'NONE', #3836, .T. ) ;
#5771=CARTESIAN_POINT ( 'NONE',  ( -3.987046614173229475, 3.845309131478920506, 8.397573164612470720 ) ) ;
#5785=ADVANCED_FACE ( 'NONE', ( #749, #3241 ), #116, .T. ) ;
#5788=CARTESIAN_POINT ( 'NONE',  ( 3.987953385826774166, 3.853790179939030391, 8.059880408514990435 ) ) ;
#5791=CARTESIAN_POINT ( 'NONE',  ( 3.987953385826772390, 3.876126805297290812, 8.413336896757332539 ) ) ;
#5811=CARTESIAN_POINT ( 'NONE',  ( -3.987046614173229919, 4.046209851938014523, 8.059880408515109451 ) ) ;
#5812=CARTESIAN_POINT ( 'NONE',  ( -3.987046614173229475, 3.793298628414998763, 8.349863190998451756 ) ) ;
#5814=CARTESIAN_POINT ( 'NONE',  ( -3.987046614173228587, 4.225666661560477877, 8.231249998505111520 ) ) ;
#5837=CARTESIAN_POINT ( 'NONE',  ( 4.462953385826773811, 3.674333370316265945, 8.231249998505111520 ) ) ;
#5860=CARTESIAN_POINT ( 'NONE',  ( -3.987046614173229475, 3.787345657127929588, 8.341552593656997416 ) ) ;
#5876=CARTESIAN_POINT ( 'NONE',  ( 3.987953385826774166, 3.756917219824144283, 8.194756059061692355 ) ) ;
#5880=CARTESIAN_POINT ( 'NONE',  ( 3.987953385826772390, 4.145406495827570481, 8.255194476359251965 ) ) ;
#5893=CARTESIAN_POINT ( 'NONE',  ( -3.987046614173228143, 3.999111350888635563, 8.423148454254917539 ) ) ;
#5896=ORIENTED_EDGE ( 'NONE', *, *, #879, .F. ) ;
#5910=CARTESIAN_POINT ( 'NONE',  ( 3.987953385826771946, 3.674333370316265501, 7.679916707260901809 ) ) ;
#5912=CARTESIAN_POINT ( 'NONE',  ( 3.987953385826772834, 4.142924502496692085, 8.268572589389476590 ) ) ;
#5958=CARTESIAN_POINT ( 'NONE',  ( 3.987953385826771946, 4.142138515950337663, 8.272475195627956523 ) ) ;
#6004=CARTESIAN_POINT ( 'NONE',  ( -3.987046614173229475, 4.123102181196484750, 8.137838423722035586 ) ) ;
#6007=ORIENTED_EDGE ( 'NONE', *, *, #1970, .T. ) ;
#6045=CARTESIAN_POINT ( 'NONE',  ( -3.987046614173228587, 4.012112954394242870, 8.044773094730338414 ) ) ;
#6057=CARTESIAN_POINT ( 'NONE',  ( 4.383786719160104539, 4.383999996532199184, 8.231249998505111520 ) ) ;
#6065=CARTESIAN_POINT ( 'NONE',  ( -4.382879947506562068, 4.383999996532200960, 8.231249998505111520 ) ) ;
#6071=CARTESIAN_POINT ( 'NONE',  ( -4.462046614173229564, 3.753500037801647871, 7.838250042231664771 ) ) ;
#6139=CARTESIAN_POINT ( 'NONE',  ( -4.382879947506561180, 3.516000035344543306, 7.363250037317454755 ) ) ;
#6142=CARTESIAN_POINT ( 'NONE',  ( 4.462953385826773811, 3.674333370316266389, 8.231249998505111520 ) ) ;
#6173=EDGE_LOOP ( 'NONE', ( #1530, #3713 ) ) ;
#6175=DIRECTION ( 'NONE',  ( -1.000000000000000000, 0.000000000000000000, 0.000000000000000000 ) ) ;
#6200=CARTESIAN_POINT ( 'NONE',  ( 3.987953385826773278, 4.133273763909712351, 8.160372747217021328 ) ) ;
#6226=PLANE ( 'NONE',  #559 ) ;
#6237=DIRECTION ( 'NONE',  ( 0.000000000000000000, 0.000000000000000000, 1.000000000000000000 ) ) ;
#6263=CARTESIAN_POINT ( 'NONE',  ( -3.987046614173229475, 3.766991497692385948, 8.159690390570178309 ) ) ;
#6274=CARTESIAN_POINT ( 'NONE',  ( 4.462953385826772035, 3.753500037802128375, 8.231249998505111520 ) ) ;
#6275=CARTESIAN_POINT ( 'NONE',  ( 4.462953385826773811, 4.225666661560476101, 8.231249998505111520 ) ) ;
#6287=ORIENTED_EDGE ( 'NONE', *, *, #5247, .T. ) ;
#6306=CARTESIAN_POINT ( 'NONE',  ( -3.987046614173228143, 3.839697420785793458, 8.068595639695207211 ) ) ;
#6325=CARTESIAN_POINT ( 'NONE',  ( 3.987953385826772390, 3.898199183956782221, 8.041502862977342403 ) ) ;
#6327=CARTESIAN_POINT ( 'NONE',  ( 3.987953385826772390, 3.950000015938371689, 8.231249998505111520 ) ) ;
#6337=CARTESIAN_POINT ( 'NONE',  ( 4.462953385826772035, 4.146499994074615003, 8.231249998505111520 ) ) ;
#6368=CARTESIAN_POINT ( 'NONE',  ( 3.987953385826774166, 3.887887077482501397, 8.044773094730341967 ) ) ;
#6371=CARTESIAN_POINT ( 'NONE',  ( 3.987953385826772390, 3.773847781579248828, 8.318774035908578668 ) ) ;
#6390=CARTESIAN_POINT ( 'NONE',  ( -3.987046614173229919, 4.033008582717316770, 8.409411560744450398 ) ) ;
#6392=CARTESIAN_POINT ( 'NONE',  ( -3.987046614173228587, 4.146499994074616779, 8.231249998505111520 ) ) ;
#6410=CARTESIAN_POINT ( 'NONE',  ( 3.987953385826772390, 3.761880377346017656, 8.173848920211581159 ) ) ;
#6424=PRODUCT_DEFINITION ( 'UNKNOWN', '', #8153, #7792 ) ;
#6429=CARTESIAN_POINT ( 'NONE',  ( -3.987046614173228143, 4.021559623873138811, 8.048241480259026304 ) ) ;
#6430=LINE ( 'NONE', #143, #7447 ) ;
#6431=CARTESIAN_POINT ( 'NONE',  ( -3.987046614173229475, 4.139745409976819168, 8.283055230728985308 ) ) ;
#6453=CARTESIAN_POINT ( 'NONE',  ( 3.987953385826772390, 3.787345657128307508, 8.120947403352559490 ) ) ;
#6457=CARTESIAN_POINT ( 'NONE',  ( 3.987953385826773278, 4.146499994074616779, 8.243275897752392112 ) ) ;
#6472=CARTESIAN_POINT ( 'NONE',  ( 4.462953385826772035, 3.753500037802128375, 8.231249998505111520 ) ) ;
#6477=CARTESIAN_POINT ( 'NONE',  ( -3.987046614173229475, 3.919106724554535681, 8.426027723965566096 ) ) ;
#6493=ORIENTED_EDGE ( 'NONE', *, *, #2305, .F. ) ;
#6504=CARTESIAN_POINT ( 'NONE',  ( 3.987953385826772390, 4.028498573891106105, 8.411512280006094855 ) ) ;
#6526=CARTESIAN_POINT ( 'NONE',  ( -3.987046614173229919, 3.769836505190808928, 8.309711754443199538 ) ) ;
#6546=CARTESIAN_POINT ( 'NONE',  ( 4.462953385826771147, 4.146499994074616779, 7.838250042232624892 ) ) ;
#6548=CARTESIAN_POINT ( 'NONE',  ( 3.987953385826772390, 4.100522301782647538, 8.357885377187420417 ) ) ;
#6555=ADVANCED_FACE ( 'NONE', ( #1179 ), #3680, .T. ) ;
#6563=ADVANCED_FACE ( 'NONE', ( #8036 ), #7071, .T. ) ;
#6567=CARTESIAN_POINT ( 'NONE',  ( -3.987046614173229475, 4.121369605927847957, 8.327459834506157677 ) ) ;
#6568=VERTEX_POINT ( 'NONE', #3791 ) ;
#6588=CARTESIAN_POINT ( 'NONE',  ( 3.987953385826772390, 3.872296061808989442, 8.411747167338544884 ) ) ;
#6591=CARTESIAN_POINT ( 'NONE',  ( -3.987046614173228143, 4.028498573889014445, 8.050987717002875854 ) ) ;
#6639=ORIENTED_EDGE ( 'NONE', *, *, #4329, .F. ) ;
#6652=( BOUNDED_CURVE ( )  B_SPLINE_CURVE ( 3, ( #2348, #6071, #1076, #2907 ),
 .UNSPECIFIED., .F., .F. ) 
 B_SPLINE_CURVE_WITH_KNOTS ( ( 4, 4 ),
 ( 0.000000000000000000, 1.000000000000000000 ),
 .UNSPECIFIED. ) 
 CURVE ( )  GEOMETRIC_REPRESENTATION_ITEM ( )  RATIONAL_B_SPLINE_CURVE ( ( 1.000000000000000000, 0.3333333333333334259, 0.3333333333333334259, 1.000000000000000000 ) ) 
 REPRESENTATION_ITEM ( '' )  );
#6666=CARTESIAN_POINT ( 'NONE',  ( -3.987046614173228587, 3.900888680994070157, 8.039351542753340851 ) ) ;
#6679=CARTESIAN_POINT ( 'NONE',  ( -3.987046614173229031, 3.674333370316265501, 7.679916707260901809 ) ) ;
#6683=CARTESIAN_POINT ( 'NONE',  ( 3.987953385826771946, 4.225666661560477877, 8.782583289749322120 ) ) ;
#6687=CARTESIAN_POINT ( 'NONE',  ( -4.066213280839896527, 4.383999996532201848, 8.231249998505111520 ) ) ;
#6700=B_SPLINE_CURVE_WITH_KNOTS ( 'NONE', 3,
 ( #736, #4416, #1307, #7570, #2580, #4376 ),
 .UNSPECIFIED., .F., .F.,
 ( 4, 2, 4 ),
 ( 0.000000000000000000, 0.5000000000000000000, 1.000000000000000000 ),
 .UNSPECIFIED. ) ;
#6707=CARTESIAN_POINT ( 'NONE',  ( -3.987046614173228587, 3.950000015938371689, 8.543749986456024459 ) ) ;
#6715=CARTESIAN_POINT ( 'NONE',  ( 4.067120052493438997, 3.516000035344542418, 9.099249959692771839 ) ) ;
#6743=CLOSED_SHELL ( 'NONE', ( #6555, #2379, #5785, #2999, #4779, #5069, #6563, #7849, #7475, #959 ) ) ;
#6755=CARTESIAN_POINT ( 'NONE',  ( -3.987046614173229031, 3.753500037802126599, 7.838250042232624004 ) ) ;
#6767=CARTESIAN_POINT ( 'NONE',  ( -4.462046614173230452, 3.674333370316265057, 8.782583289749325672 ) ) ;
#6791=CARTESIAN_POINT ( 'NONE',  ( -3.987046614173228587, 3.753500037802127043, 8.231249998505111520 ) ) ;
#6809=PRODUCT ( 'bench vise10-', 'bench vise10-', '', ( #8179 ) ) ;
#6856=CARTESIAN_POINT ( 'NONE',  ( 3.987953385826772390, 4.121369605928006052, 8.135040162505021044 ) ) ;
#6878=DIRECTION ( 'NONE',  ( 0.000000000000000000, 0.000000000000000000, 1.000000000000000000 ) ) ;
#6895=VERTEX_POINT ( 'NONE', #4108 ) ;
#6914=CARTESIAN_POINT ( 'NONE',  ( 4.462953385826771147, 3.753500037802128375, 8.231249998505111520 ) ) ;
#6919=CARTESIAN_POINT ( 'NONE',  ( -3.987046614173229475, 3.823364637257366638, 8.080727712660298323 ) ) ;
#6924=CARTESIAN_POINT ( 'NONE',  ( -3.987046614173228587, 3.753500037802127043, 8.231249998505111520 ) ) ;
#6939=CARTESIAN_POINT ( 'NONE',  ( 3.987953385826772390, 3.880579470499919026, 8.047419037877352466 ) ) ;
#6944=CARTESIAN_POINT ( 'NONE',  ( 3.987953385826772390, 3.778630425948584559, 8.327459834505681613 ) ) ;
#6982=CARTESIAN_POINT ( 'NONE',  ( 3.987953385826772390, 3.879123177173087633, 8.047976087269148593 ) ) ;
#7007=CARTESIAN_POINT ( 'NONE',  ( -3.987046614173230363, 3.880579470500146844, 8.415080959133112160 ) ) ;
#7009=CARTESIAN_POINT ( 'NONE',  ( -4.066213280839894750, 4.383999996532201848, 9.099249959692773615 ) ) ;
#7024=VERTEX_POINT ( 'NONE', #6707 ) ;
#7028=CARTESIAN_POINT ( 'NONE',  ( 3.987953385826771058, 3.919106724552877452, 8.036472273046371129 ) ) ;
#7051=CARTESIAN_POINT ( 'NONE',  ( -3.987046614173228587, 4.076635394620980790, 8.381772284349393587 ) ) ;
#7053=CARTESIAN_POINT ( 'NONE',  ( -4.382879947506562068, 4.383999996532200960, 8.231249998505111520 ) ) ;
#7059=CARTESIAN_POINT ( 'NONE',  ( -4.462046614173229564, 4.146499994075099060, 8.624249954778562710 ) ) ;
#7067=CARTESIAN_POINT ( 'NONE',  ( 3.987953385826774166, 3.974973691467368120, 8.034752674066883316 ) ) ;
#7069=CARTESIAN_POINT ( 'NONE',  ( 3.987953385826772390, 4.131461189140908985, 8.306660907471565380 ) ) ;
#7071=( BOUNDED_SURFACE ( )  B_SPLINE_SURFACE ( 3, 3, ( 
 ( #8165, #4159, #4199, #4865 ),
 ( #1757, #2334, #6683, #3556 ),
 ( #2497, #6715, #4907, #8124 ),
 ( #1102, #3645, #4828, #6057 ),
 ( #6142, #2464, #4984, #4409 ),
 ( #6914, #5725, #3901, #5181 ) ),
 .UNSPECIFIED., .F., .F., .F. ) 
 B_SPLINE_SURFACE_WITH_KNOTS ( ( 4, 2, 4 ),
 ( 4, 4 ),
 ( 0.000000000000000000, 0.5000000000000000000, 1.000000000000000000 ),
 ( 0.000000000000000000, 1.000000000000000000 ),
 .UNSPECIFIED. ) 
 GEOMETRIC_REPRESENTATION_ITEM ( )  RATIONAL_B_SPLINE_SURFACE ( (
 ( 1.000000000000000000, 0.3333333333333332038, 0.3333333333333332038, 1.000000000000000000),
 ( 1.000000000000000000, 0.3333333333333332038, 0.3333333333333332038, 1.000000000000000000),
 ( 1.000000000000000000, 0.3333333333333332038, 0.3333333333333332038, 1.000000000000000000),
 ( 1.000000000000000000, 0.3333333333333332038, 0.3333333333333332038, 1.000000000000000000),
 ( 1.000000000000000000, 0.3333333333333332038, 0.3333333333333332038, 1.000000000000000000),
 ( 1.000000000000000000, 0.3333333333333332038, 0.3333333333333332038, 1.000000000000000000) ) ) 
 REPRESENTATION_ITEM ( '' )  SURFACE ( )  );
#7087=CARTESIAN_POINT ( 'NONE',  ( -3.987046614173228587, 3.882766440201689484, 8.415903052206909152 ) ) ;
#7098=CARTESIAN_POINT ( 'NONE',  ( 4.462953385826772923, 3.753500037801648759, 8.624249954778562710 ) ) ;
#7108=CARTESIAN_POINT ( 'NONE',  ( 3.987953385826772390, 3.878440408003577922, 8.048241480259036962 ) ) ;
#7114=CARTESIAN_POINT ( 'NONE',  ( 3.987953385826771946, 4.135047251020852244, 8.297661934733794098 ) ) ;
#7127=CARTESIAN_POINT ( 'NONE',  ( -3.987046614173228143, 3.789313681612213713, 8.344403569825507461 ) ) ;
#7154=CARTESIAN_POINT ( 'NONE',  ( 3.987953385826771946, 4.001800847919377624, 8.420997134034163167 ) ) ;
#7171=CARTESIAN_POINT ( 'NONE',  ( -3.987046614173228587, 4.130262297440223662, 8.309748556456774793 ) ) ;
#7195=CARTESIAN_POINT ( 'NONE',  ( 3.987953385826771946, 4.021559623872877687, 8.414258516751351280 ) ) ;
#7196=EDGE_CURVE ( 'NONE', #6895, #5506, #2591, .T. ) ;
#7200=CARTESIAN_POINT ( 'NONE',  ( -3.987046614173228587, 3.950000015938371689, 7.918750010554200358 ) ) ;
#7215=VERTEX_POINT ( 'NONE', #832 ) ;
#7220=EDGE_LOOP ( 'NONE', ( #335, #6639 ) ) ;
#7233=CARTESIAN_POINT ( 'NONE',  ( 4.462953385826773811, 3.674333370316265501, 7.679916707260901809 ) ) ;
#7272=AXIS2_PLACEMENT_3D ( 'NONE', #3736, #6237, #5618 ) ;
#7292=CARTESIAN_POINT ( 'NONE',  ( -3.987046614173227699, 4.142138515950292366, 8.190024801382838504 ) ) ;
#7309=DIRECTION ( 'NONE',  ( -0.000000000000000000, 0.000000000000000000, -1.000000000000000000 ) ) ;
#7332=ORIENTED_EDGE ( 'NONE', *, *, #4329, .T. ) ;
#7334=CARTESIAN_POINT ( 'NONE',  ( -3.987046614173228587, 4.146499994074616779, 8.231249998505111520 ) ) ;
#7351=ORIENTED_EDGE ( 'NONE', *, *, #3644, .F. ) ;
#7355=SHAPE_REPRESENTATION ( 'bench vise10-', ( #7272 ), #456 ) ;
#7387=CARTESIAN_POINT ( 'NONE',  ( -4.462046614173229564, 3.753500037802126599, 7.838250042232624004 ) ) ;
#7391=CARTESIAN_POINT ( 'NONE',  ( 4.476342532109287120, 3.950000015938371689, 8.231249998505111520 ) ) ;
#7402=CARTESIAN_POINT ( 'NONE',  ( -4.462046614173229564, 4.146499994074616779, 8.624249954777603477 ) ) ;
#7424=EDGE_CURVE ( 'NONE', #3656, #7024, #820, .T. ) ;
#7426=CARTESIAN_POINT ( 'NONE',  ( 3.987953385826772390, 4.076635394618645769, 8.080727712659717454 ) ) ;
#7438=CARTESIAN_POINT ( 'NONE',  ( -3.987046614173228587, 4.225666661560477877, 8.231249998505111520 ) ) ;
#7445=DIRECTION ( 'NONE',  ( 0.000000000000000000, 0.000000000000000000, 1.000000000000000000 ) ) ;
#7447=VECTOR ( 'NONE', #2660, 39.37007874015748143 ) ;
#7475=ADVANCED_FACE ( 'NONE', ( #3501 ), #6226, .T. ) ;
#7493=ORIENTED_EDGE ( 'NONE', *, *, #3599, .T. ) ;
#7496=CARTESIAN_POINT ( 'NONE',  ( -3.987046614173228587, 3.753500037802127043, 8.231249998505111520 ) ) ;
#7516=CARTESIAN_POINT ( 'NONE',  ( -4.462046614173229564, 3.753500037802127043, 8.231249998505111520 ) ) ;
#7526=CARTESIAN_POINT ( 'NONE',  ( -3.987046614173229475, 3.765347506452386916, 8.164015047692851468 ) ) ;
#7546=EDGE_CURVE ( 'NONE', #2207, #1601, #6700, .T. ) ;
#7548=CARTESIAN_POINT ( 'NONE',  ( 3.987953385826772390, 4.134652525424356462, 8.164015047692018356 ) ) ;
#7562=EDGE_LOOP ( 'NONE', ( #1634, #5246, #287, #3605 ) ) ;
#7570=CARTESIAN_POINT ( 'NONE',  ( -4.066213280839896527, 3.516000035344541974, 8.231249998505111520 ) ) ;
#7594=CARTESIAN_POINT ( 'NONE',  ( 3.987953385826772390, 3.766991497692264712, 8.302809606439794265 ) ) ;
#7610=CARTESIAN_POINT ( 'NONE',  ( -3.987046614173229031, 4.146499994074616779, 8.624249954777603477 ) ) ;
#7628=CARTESIAN_POINT ( 'NONE',  ( 3.987953385826771946, 4.027703970067857853, 8.050752829671607103 ) ) ;
#7631=CARTESIAN_POINT ( 'NONE',  ( 3.987953385826772390, 3.836846444618124075, 8.391936332831416934 ) ) ;
#7641=CARTESIAN_POINT ( 'NONE',  ( 4.462953385826773811, 3.674333370316266389, 8.231249998505111520 ) ) ;
#7646=DIRECTION ( 'NONE',  ( -1.000000000000000000, 0.000000000000000000, 0.000000000000000000 ) ) ;
#7648=CARTESIAN_POINT ( 'NONE',  ( -3.987046614173230363, 4.068613208432641848, 8.387951386028037248 ) ) ;
#7668=EDGE_CURVE ( 'NONE', #231, #1601, #1127, .T. ) ;
#7669=CARTESIAN_POINT ( 'NONE',  ( 3.987953385826773278, 3.783676849830679867, 8.335940882964230525 ) ) ;
#7691=CARTESIAN_POINT ( 'NONE',  ( -3.987046614173227699, 3.763524128032367688, 8.169134493242211192 ) ) ;
#7694=CARTESIAN_POINT ( 'NONE',  ( -3.987046614173229475, 3.768538842735829952, 8.306660907471561828 ) ) ;
#7716=CARTESIAN_POINT ( 'NONE',  ( 3.987953385826773278, 4.079363137581865750, 8.379777743322501138 ) ) ;
#7733=CARTESIAN_POINT ( 'NONE',  ( -3.987046614173228587, 4.136475903844373470, 8.293365503768981739 ) ) ;
#7752=CARTESIAN_POINT ( 'NONE',  ( 3.987953385826772390, 3.799477730091489036, 8.104614619826481459 ) ) ;
#7765=CARTESIAN_POINT ( 'NONE',  ( 4.067120052493439886, 3.516000035344543306, 8.231249998505111520 ) ) ;
#7770=CARTESIAN_POINT ( 'NONE',  ( -3.987046614173227699, 4.118031710298097892, 8.333174882269599237 ) ) ;
#7792=DESIGN_CONTEXT ( 'detailed design', #1684, 'design' ) ;
#7793=APPLICATION_CONTEXT ( 'configuration controlled 3d designs of mechanical parts and assemblies' ) ;
#7818=CARTESIAN_POINT ( 'NONE',  ( -3.987046614173228587, 4.051974939360865058, 8.399350079849284612 ) ) ;
#7820=FACE_OUTER_BOUND ( 'NONE', #4145, .T. ) ;
#7844=CARTESIAN_POINT ( 'NONE',  ( 3.987953385826772390, 4.020876854703599790, 8.414523909741193464 ) ) ;
#7849=ADVANCED_FACE ( 'NONE', ( #4678 ), #7952, .T. ) ;
#7850=CARTESIAN_POINT ( 'NONE',  ( -3.987046614173229475, 4.142615650101483027, 8.192364704391877694 ) ) ;
#7878=LENGTH_MEASURE_WITH_UNIT ( LENGTH_MEASURE( 0.02539999999999999897 ), #4592 );
#7884=UNCERTAINTY_MEASURE_WITH_UNIT (LENGTH_MEASURE( 1.000000000000000082E-05 ), #4708, 'distance_accuracy_value', 'NONE');
#7926=CARTESIAN_POINT ( 'NONE',  ( -3.987046614173229919, 4.051924899701968563, 8.063218304145049586 ) ) ;
#7944=CARTESIAN_POINT ( 'NONE',  ( -4.462046614173230452, 4.225666661560478765, 7.679916707260899145 ) ) ;
#7952=( BOUNDED_SURFACE ( )  B_SPLINE_SURFACE ( 3, 3, ( 
 ( #915, #3416, #2191, #1574 ),
 ( #3976, #829, #5910, #338 ),
 ( #3455, #3332, #298, #2720 ),
 ( #4055, #4639, #4019, #218 ),
 ( #5244, #2107, #7233, #5837 ),
 ( #3373, #6546, #5209, #1496 ) ),
 .UNSPECIFIED., .F., .F., .T. ) 
 B_SPLINE_SURFACE_WITH_KNOTS ( ( 4, 2, 4 ),
 ( 4, 4 ),
 ( 0.000000000000000000, 0.5000000000000000000, 1.000000000000000000 ),
 ( 0.000000000000000000, 1.000000000000000000 ),
 .UNSPECIFIED. ) 
 GEOMETRIC_REPRESENTATION_ITEM ( )  RATIONAL_B_SPLINE_SURFACE ( (
 ( 1.000000000000000000, 0.3333333333333334259, 0.3333333333333334259, 1.000000000000000000),
 ( 1.000000000000000000, 0.3333333333333334259, 0.3333333333333334259, 1.000000000000000000),
 ( 1.000000000000000000, 0.3333333333333334259, 0.3333333333333334259, 1.000000000000000000),
 ( 1.000000000000000000, 0.3333333333333334259, 0.3333333333333334259, 1.000000000000000000),
 ( 1.000000000000000000, 0.3333333333333334259, 0.3333333333333334259, 1.000000000000000000),
 ( 1.000000000000000000, 0.3333333333333334259, 0.3333333333333334259, 1.000000000000000000) ) ) 
 REPRESENTATION_ITEM ( '' )  SURFACE ( )  );
#7953=ADVANCED_BREP_SHAPE_REPRESENTATION ( '', ( #2701, #7272 ), #456 ) ;
#7962=ORIENTED_EDGE ( 'NONE', *, *, #4323, .F. ) ;
#7976=CARTESIAN_POINT ( 'NONE',  ( -3.987046614173228587, 4.054690900397527109, 8.064926832397588896 ) ) ;
#7994=CARTESIAN_POINT ( 'NONE',  ( -4.462046614173230452, 3.674333370316265057, 7.679916707260899145 ) ) ;
#8020=ORIENTED_EDGE ( 'NONE', *, *, #7196, .T. ) ;
#8036=FACE_OUTER_BOUND ( 'NONE', #1831, .T. ) ;
#8061=CARTESIAN_POINT ( 'NONE',  ( 3.987953385826771946, 4.107055349781281173, 8.112380013460960271 ) ) ;
#8107=CARTESIAN_POINT ( 'NONE',  ( 3.987953385826774166, 4.063153587258190313, 8.070563664178681762 ) ) ;
#8124=CARTESIAN_POINT ( 'NONE',  ( 4.067120052493439886, 4.383999996532200072, 8.231249998505111520 ) ) ;
#8143=CARTESIAN_POINT ( 'NONE',  ( 4.067120052493439886, 4.383999996532200072, 8.231249998505111520 ) ) ;
#8149=CARTESIAN_POINT ( 'NONE',  ( 3.987953385826772390, 4.146499994074616779, 8.218759808174304737 ) ) ;
#8153=PRODUCT_DEFINITION_FORMATION_WITH_SPECIFIED_SOURCE ( 'ANY', '', #6809, .NOT_KNOWN. ) ;
#8155=CARTESIAN_POINT ( 'NONE',  ( 3.987953385826771946, 3.765347506452387805, 8.298484949317723292 ) ) ;
#8165=CARTESIAN_POINT ( 'NONE',  ( 3.987953385826771946, 3.753500037802128375, 8.231249998505111520 ) ) ;
#8173=CARTESIAN_POINT ( 'NONE',  ( -4.462046614173229564, 3.950000015938371689, 8.231249998505111520 ) ) ;
#8175=CARTESIAN_POINT ( 'NONE',  ( -4.462046614173230452, 4.225666661560478765, 8.782583289749325672 ) ) ;
#8179=MECHANICAL_CONTEXT ( 'NONE', #7793, 'mechanical' ) ;
#8184=CARTESIAN_POINT ( 'NONE',  ( 3.987953385826771946, 4.225666661560476101, 8.231249998505111520 ) ) ;
#8213=COLOUR_RGB('Sky Blue', 0.40784314, 0.44705882, 0.49803922);
#8214=FILL_AREA_STYLE_COLOUR('',#8213);
#8215=FILL_AREA_STYLE('',(#8214));
#8216=SURFACE_STYLE_FILL_AREA(#8215);
#8217=SURFACE_SIDE_STYLE('',(#8216));
#8218=SURFACE_STYLE_USAGE(.BOTH.,#8217);
#8219=PRESENTATION_STYLE_ASSIGNMENT((#8218));
#8261=STYLED_ITEM('',(#8219),#2701);
#8262=MECHANICAL_DESIGN_GEOMETRIC_PRESENTATION_REPRESENTATION('',(#8261),#456);
ENDSEC;
END-ISO-10303-21;
